ISO-10303-21;
HEADER;
FILE_DESCRIPTION (('STEP AP214'),
    '1' );
FILE_NAME ('hex flange nut gradea_iso_ISO - 4161 - M12 - N.step',
    '2026-10-22T16:49:52',
    ( '' ),
    ( '' ),
    'SwSTEP 2.0',
    'SolidWorks 2026',
    '' );
FILE_SCHEMA (( 'AUTOMOTIVE_DESIGN' ));
ENDSEC;

DATA;
#6=AXIS2_PLACEMENT_3D ( 'NONE', #4882, #5186, #2714 ) ;
#14=FACE_OUTER_BOUND ( 'NONE', #5143, .T. ) ;
#17=CARTESIAN_POINT ( 'NONE',  ( 5.999999999999999112, -6.928203230275514102, -8.505011083697299412 ) ) ;
#21=CARTESIAN_POINT ( 'NONE',  ( 9.000000000000000000, -5.196152422706636465, -8.935996291721336249 ) ) ;
#26=EDGE_LOOP ( 'NONE', ( #4357, #319, #2508, #4041 ) ) ;
#31=CARTESIAN_POINT ( 'NONE',  ( 9.417977369734737536, -4.954833075775112228, -9.021743230619932774 ) ) ;
#34=DIRECTION ( 'NONE',  ( 1.000000000000000000, 0.000000000000000000, 0.000000000000000000 ) ) ;
#43=CARTESIAN_POINT ( 'NONE',  ( 8.716942385998452281, -5.934590066575466061, -9.518277236634762772 ) ) ;
#51=VECTOR ( 'NONE', #3265, 1000.000000000000000 ) ;
#56=CARTESIAN_POINT ( 'NONE',  ( -5.303004762135290484, 7.330613618480585458, -8.460795847313656637 ) ) ;
#68=SURFACE_STYLE_FILL_AREA ( #524 ) ;
#73=DIRECTION ( 'NONE',  ( 0.000000000000000000, 0.000000000000000000, -1.000000000000000000 ) ) ;
#86=CARTESIAN_POINT ( 'NONE',  ( -0.3334815747005946962, -10.58484052233643702, -9.543752552345290852 ) ) ;
#87=CARTESIAN_POINT ( 'NONE',  ( -17.99999999999999645, -3.469446951953614189E-15, 0.000000000000000000 ) ) ;
#90=CARTESIAN_POINT ( 'NONE',  ( 0.000000000000000000, 0.000000000000000000, -12.00000000000000000 ) ) ;
#91=CARTESIAN_POINT ( 'NONE',  ( 5.099999999999999645, 0.000000000000000000, -0.6301867843887398735 ) ) ;
#94=CARTESIAN_POINT ( 'NONE',  ( 7.780966735391740663, 5.899961606179080498, -9.200452032548549042 ) ) ;
#96=CARTESIAN_POINT ( 'NONE',  ( 3.148120153201419136, -9.125992800952634099, -9.189707035345831443 ) ) ;
#100=CARTESIAN_POINT ( 'NONE',  ( 0.000000000000000000, 0.000000000000000000, 0.000000000000000000 ) ) ;
#105=CARTESIAN_POINT ( 'NONE',  ( 9.506737344437272696, -5.488717364925930653, -9.686084310752812954 ) ) ;
#107=CARTESIAN_POINT ( 'NONE',  ( -3.715831927071960639, 8.246968282054856658, 1.905824131322174974E-15 ) ) ;
#113=CARTESIAN_POINT ( 'NONE',  ( 9.333481574700595473, 5.003616745783458164, -9.543752552345289075 ) ) ;
#123=ORIENTED_EDGE ( 'NONE', *, *, #1408, .F. ) ;
#124=DIRECTION ( 'NONE',  ( 1.224646799147353207E-16, 1.000000000000000000, 0.000000000000000000 ) ) ;
#131=CARTESIAN_POINT ( 'NONE',  ( -8.999999999999998224, 4.786605659887710473, -1.023509873932516578 ) ) ;
#133=DIRECTION ( 'NONE',  ( 1.000000000000000000, 0.000000000000000000, 0.000000000000000000 ) ) ;
#135=ORIENTED_EDGE ( 'NONE', *, *, #3214, .F. ) ;
#155=ORIENTED_EDGE ( 'NONE', *, *, #2076, .F. ) ;
#166=CARTESIAN_POINT ( 'NONE',  ( 9.000000000000000000, -5.196152422706636465, -8.935996291721336249 ) ) ;
#168=CARTESIAN_POINT ( 'NONE',  ( 8.999999999999998224, -3.085342593989931714, -0.4353033105082919074 ) ) ;
#171=CARTESIAN_POINT ( 'NONE',  ( 5.010000000000002451, 0.000000000000000000, -0.6932054628276118624 ) ) ;
#173=CARTESIAN_POINT ( 'NONE',  ( 12.38940648156203927, 1.517264699098042146E-15, -10.20000000000000107 ) ) ;
#174=DIRECTION ( 'NONE',  ( -1.000000000000000000, 0.000000000000000000, 0.000000000000000000 ) ) ;
#175=CARTESIAN_POINT ( 'NONE',  ( 8.999999999999998224, 5.582890641074283344, -9.544071791823135698 ) ) ;
#176=CARTESIAN_POINT ( 'NONE',  ( 7.500000000000000000, 6.062177826491069510, -8.667800885990208926 ) ) ;
#180=CARTESIAN_POINT ( 'NONE',  ( 0.000000000000000000, 0.000000000000000000, 0.000000000000000000 ) ) ;
#182=PRODUCT_DEFINITION ( 'UNKNOWN', '', #3186, #2002 ) ;
#185=CARTESIAN_POINT ( 'NONE',  ( -9.000000000000000000, 5.196152422706629359, -8.935996291721334472 ) ) ;
#193=FACE_OUTER_BOUND ( 'NONE', #4538, .T. ) ;
#202=ORIENTED_EDGE ( 'NONE', *, *, #4322, .T. ) ;
#209=CARTESIAN_POINT ( 'NONE',  ( -9.506737344437272696, 5.488717364925923548, -9.686084310752812954 ) ) ;
#214=CARTESIAN_POINT ( 'NONE',  ( 9.000000000000007105, -5.196152422706631135, -9.106324069981642566 ) ) ;
#221=CARTESIAN_POINT ( 'NONE',  ( -3.936978610624180419, -8.666338374798538524, -9.138972935415381471 ) ) ;
#222=CARTESIAN_POINT ( 'NONE',  ( 4.105894441359817293, 8.021765584429983775, 1.987139294258588595E-15 ) ) ;
#228=AXIS2_PLACEMENT_3D ( 'NONE', #622, #648, #2683 ) ;
#229=MECHANICAL_DESIGN_GEOMETRIC_PRESENTATION_REPRESENTATION('',(#3546),#1970);
#230=CARTESIAN_POINT ( 'NONE',  ( 9.000000000000000000, -1.974011471328773748, -8.465140122390733879 ) ) ;
#233=EDGE_CURVE ( 'NONE', #932, #4959, #723, .T. ) ;
#235=ORIENTED_EDGE ( 'NONE', *, *, #3529, .T. ) ;
#240=FACE_OUTER_BOUND ( 'NONE', #4695, .T. ) ;
#244=CARTESIAN_POINT ( 'NONE',  ( -6.177322775498885754, -6.825825878106156708, -8.969375302469426714 ) ) ;
#250=CARTESIAN_POINT ( 'NONE',  ( 9.000000000000000000, -4.368650009232623255, -0.8589767385557531831 ) ) ;
#251=CARTESIAN_POINT ( 'NONE',  ( 0.000000000000000000, 0.000000000000000000, 0.000000000000000000 ) ) ;
#252=CARTESIAN_POINT ( 'NONE',  ( -0.7813822207450746848, 10.51618336147351584, -9.518202542148552325 ) ) ;
#256=CARTESIAN_POINT ( 'NONE',  ( 8.999999999999998224, 3.726892940488169881, -9.220324059310399889 ) ) ;
#263=DIRECTION ( 'NONE',  ( 0.000000000000000000, 0.000000000000000000, 1.000000000000000000 ) ) ;
#264=ADVANCED_FACE ( 'NONE', ( #307 ), #2257, .T. ) ;
#265=EDGE_LOOP ( 'NONE', ( #2371, #2953, #3859, #3002, #619 ) ) ;
#266=EDGE_CURVE ( 'NONE', #4086, #2529, #4435, .T. ) ;
#267=ORIENTED_EDGE ( 'NONE', *, *, #3062, .T. ) ;
#268=CARTESIAN_POINT ( 'NONE',  ( -12.07201791628681420, 1.497830254570528423E-15, -12.00000000000000178 ) ) ;
#270=CARTESIAN_POINT ( 'NONE',  ( 9.473745496805531019, 0.9193675319299579041, -9.138786188337409300 ) ) ;
#274=B_SPLINE_CURVE_WITH_KNOTS ( 'NONE', 3,
 ( #1691, #107, #2527, #1724, #4580, #2576 ),
 .UNSPECIFIED., .F., .F.,
 ( 4, 2, 4 ),
 ( 0.005333245961717295557, 0.007986067645924077585, 0.01063888933013085875 ),
 .UNSPECIFIED. ) ;
#277=CARTESIAN_POINT ( 'NONE',  ( -3.145304002162441659, -9.127642243957643231, -9.190020220263408035 ) ) ;
#290=AXIS2_PLACEMENT_3D ( 'NONE', #2542, #2961, #4599 ) ;
#292=DIRECTION ( 'NONE',  ( -0.5000000000000004441, 0.8660254037844384856, 0.000000000000000000 ) ) ;
#307=FACE_OUTER_BOUND ( 'NONE', #4376, .T. ) ;
#310=EDGE_CURVE ( 'NONE', #3078, #932, #2677, .T. ) ;
#315=( GEOMETRIC_REPRESENTATION_CONTEXT ( 3 ) GLOBAL_UNCERTAINTY_ASSIGNED_CONTEXT ( ( #477 ) ) GLOBAL_UNIT_ASSIGNED_CONTEXT ( ( #4680, #2127, #929 ) ) REPRESENTATION_CONTEXT ( 'NONE', 'WORKASPACE' ) );
#319=ORIENTED_EDGE ( 'NONE', *, *, #4633, .F. ) ;
#322=ORIENTED_EDGE ( 'NONE', *, *, #3874, .F. ) ;
#328=EDGE_CURVE ( 'NONE', #745, #5291, #1071, .T. ) ;
#331=DIRECTION ( 'NONE',  ( 0.000000000000000000, 0.000000000000000000, -1.000000000000000000 ) ) ;
#335=SHAPE_DEFINITION_REPRESENTATION ( #2409, #1634 ) ;
#340=CARTESIAN_POINT ( 'NONE',  ( -3.148120153201420912, 9.125992800952626993, -9.189707035345829667 ) ) ;
#346=EDGE_LOOP ( 'NONE', ( #4288, #3328, #1002, #1263, #1161 ) ) ;
#361=CARTESIAN_POINT ( 'NONE',  ( -2.352990130084610634E-16, 10.39230484541326582, -8.935996291721336249 ) ) ;
#368=CARTESIAN_POINT ( 'NONE',  ( -4.500000000000001776, 7.794228634059948035, -8.419403919045800322 ) ) ;
#369=ORIENTED_EDGE ( 'NONE', *, *, #1898, .T. ) ;
#378=CARTESIAN_POINT ( 'NONE',  ( 8.603171985749828110, -5.425261183555956102, -8.848996304169093108 ) ) ;
#382=CARTESIAN_POINT ( 'NONE',  ( -9.497981232281496489, 4.582241663078505667, -9.518359232022067573 ) ) ;
#383=CONICAL_SURFACE ( 'NONE', #1593, 5.010000000000002451, 0.9599310885968808105 ) ;
#391=EDGE_CURVE ( 'NONE', #2814, #4086, #2436, .T. ) ;
#402=CARTESIAN_POINT ( 'NONE',  ( 0.000000000000000000, 0.000000000000000000, -11.97459999999999880 ) ) ;
#403=B_SPLINE_CURVE_WITH_KNOTS ( 'NONE', 3,
 ( #411, #4225, #176, #667, #3919, #915, #1835, #3946, #2719 ),
 .UNSPECIFIED., .F., .F.,
 ( 4, 2, 1, 2, 4 ),
 ( 0.000000000000000000, 0.002598076211353316737, 0.005196152422706633474, 0.007794228634059948910, 0.01039230484541326521 ),
 .UNSPECIFIED. ) ;
#411=CARTESIAN_POINT ( 'NONE',  ( 9.000000000000000000, 5.196152422706629359, -8.935996291721334472 ) ) ;
#412=CARTESIAN_POINT ( 'NONE',  ( 9.506737344437272696, 5.488717364925924436, -9.686084310752812954 ) ) ;
#415=CONICAL_SURFACE ( 'NONE', #4083, 12.38940648156203927, 1.221730476396048370 ) ;
#416=B_SPLINE_CURVE_WITH_KNOTS ( 'NONE', 3,
 ( #185, #4385, #3497, #1797, #3906, #3060, #5151, #4699, #2649 ),
 .UNSPECIFIED., .F., .F.,
 ( 4, 2, 1, 2, 4 ),
 ( 0.000000000000000000, 0.002598076211353316737, 0.005196152422706633474, 0.007794228634059951512, 0.01039230484541326521 ),
 .UNSPECIFIED. ) ;
#422=CARTESIAN_POINT ( 'NONE',  ( 4.500000000000001776, -7.794228634059955141, -8.419403919045802098 ) ) ;
#425=CARTESIAN_POINT ( 'NONE',  ( 9.058808647644763568, 5.230105611255011944, -9.269271692759767589 ) ) ;
#426=CARTESIAN_POINT ( 'NONE',  ( 9.000000000000000000, 0.2246546977803023648, 1.531435568635775407E-15 ) ) ;
#428=VERTEX_POINT ( 'NONE', #361 ) ;
#437=CARTESIAN_POINT ( 'NONE',  ( -5.284168072928043358, -7.341488986065035860, -3.941244303574257900E-15 ) ) ;
#438=PLANE ( 'NONE',  #3355 ) ;
#440=CARTESIAN_POINT ( 'NONE',  ( -1.447884101293563486, -9.556368569776052979, -0.5428950306860302888 ) ) ;
#444=ORIENTED_EDGE ( 'NONE', *, *, #762, .T. ) ;
#446=CARTESIAN_POINT ( 'NONE',  ( -0.3349232592648703211, 10.58567287930770817, -9.544071379897774321 ) ) ;
#447=CARTESIAN_POINT ( 'NONE',  ( 9.000000000000001776, 0.9001646245238089650, -0.03631462189738251384 ) ) ;
#454=DIRECTION ( 'NONE',  ( -1.000000000000000000, 0.000000000000000000, 0.000000000000000000 ) ) ;
#460=CARTESIAN_POINT ( 'NONE',  ( -6.134460314789387247, 6.850572531336530879, -8.512883888440001101 ) ) ;
#466=CARTESIAN_POINT ( 'NONE',  ( -8.999999999999996447, -5.582885416786369071, -9.544070791154714684 ) ) ;
#467=B_SPLINE_CURVE_WITH_KNOTS ( 'NONE', 3,
 ( #4058, #658, #2326, #3615, #5307, #3231, #340, #4002, #252, #2770 ),
 .UNSPECIFIED., .F., .F.,
 ( 4, 2, 2, 2, 4 ),
 ( 0.000000000000000000, 0.002766603965071789267, 0.005533207930143578535, 0.008299811895215367802, 0.01106641586028715707 ),
 .UNSPECIFIED. ) ;
#476=CARTESIAN_POINT ( 'NONE',  ( 9.416515850482076289, 4.955676884309055730, -9.021433408186453562 ) ) ;
#477=UNCERTAINTY_MEASURE_WITH_UNIT (LENGTH_MEASURE( 1.000000000000000082E-05 ), #4680, 'distance_accuracy_value', 'NONE');
#478=CARTESIAN_POINT ( 'NONE',  ( 9.000000000000001776, 4.786605659887718467, -1.023509873932519687 ) ) ;
#480=AXIS2_PLACEMENT_3D ( 'NONE', #2323, #4390, #2713 ) ;
#482=CARTESIAN_POINT ( 'NONE',  ( 0.000000000000000000, 0.000000000000000000, -10.20000000000000107 ) ) ;
#490=CARTESIAN_POINT ( 'NONE',  ( -5.287803175666994981, 7.339390258519110866, -8.964894084809513330 ) ) ;
#491=STYLED_ITEM ( 'NONE', ( #4235 ), #1615 ) ;
#492=CARTESIAN_POINT ( 'NONE',  ( 2.822677224501522808, -8.762631390014002264, -8.969375302469423161 ) ) ;
#498=CARTESIAN_POINT ( 'NONE',  ( 6.000000000000000000, 0.000000000000000000, 0.000000000000000000 ) ) ;
#499=CARTESIAN_POINT ( 'NONE',  ( -9.000000000000000000, 5.677108048117061045, -9.021434243155090016 ) ) ;
#500=( NAMED_UNIT ( * ) SI_UNIT ( $, .STERADIAN. ) SOLID_ANGLE_UNIT ( ) );
#506=CARTESIAN_POINT ( 'NONE',  ( 0.000000000000000000, 0.000000000000000000, -0.6301867843887398735 ) ) ;
#511=( BOUNDED_SURFACE ( )  B_SPLINE_SURFACE ( 3, 2, ( 
 ( #499, #2943, #860 ),
 ( #1240, #1726, #5052 ),
 ( #2101, #1290, #1311 ),
 ( #2159, #3857, #2499 ),
 ( #4628, #3833, #4581 ),
 ( #2081, #2919, #2991 ),
 ( #1332, #3779, #2528 ),
 ( #899, #466, #5078 ) ),
 .UNSPECIFIED., .F., .F., .F. ) 
 B_SPLINE_SURFACE_WITH_KNOTS ( ( 4, 2, 2, 4 ),
 ( 3, 3 ),
 ( 0.04601127232121990374, 0.05157242366991564297, 0.05435299934426351259, 0.05713357501861138221 ),
 ( 0.000000000000000000, 1.000000000000000000 ),
 .UNSPECIFIED. ) 
 GEOMETRIC_REPRESENTATION_ITEM ( )  RATIONAL_B_SPLINE_SURFACE ( (
 ( 1.000000000000000000, 0.8047781497997479327, 1.000000000000000000),
 ( 1.000000000000000000, 0.8123770896799767938, 1.000000000000000000),
 ( 1.000000000000000000, 0.8190668965778666877, 1.000000000000000000),
 ( 1.000000000000000000, 0.8191933289379096372, 1.000000000000000000),
 ( 1.000000000000000000, 0.8176087259132261975, 1.000000000000000000),
 ( 1.000000000000000000, 0.8122957709810018079, 1.000000000000000000),
 ( 1.000000000000000000, 0.8086309318960932524, 1.000000000000000000),
 ( 1.000000000000000000, 0.8047712439490427583, 1.000000000000000000) ) ) 
 REPRESENTATION_ITEM ( '' )  SURFACE ( )  );
#513=DIRECTION ( 'NONE',  ( -1.000000000000000000, 1.224646799147352468E-16, 0.000000000000000000 ) ) ;
#524=FILL_AREA_STYLE ('',( #951 ) ) ;
#527=CARTESIAN_POINT ( 'NONE',  ( 0.3968280142506481756, 10.16319608456367085, -8.848996304171389937 ) ) ;
#532=CARTESIAN_POINT ( 'NONE',  ( 6.430436718082018110, -6.679690475221758739, -0.2264046624879813563 ) ) ;
#534=EDGE_LOOP ( 'NONE', ( #2806, #1893, #3164, #1680 ) ) ;
#541=CARTESIAN_POINT ( 'NONE',  ( 0.000000000000000000, 0.000000000000000000, 0.000000000000000000 ) ) ;
#542=DIRECTION ( 'NONE',  ( 0.000000000000000000, 0.000000000000000000, -1.000000000000000000 ) ) ;
#546=CARTESIAN_POINT ( 'NONE',  ( 3.715831927071962859, -8.246968282054865540, -4.078463641029454555E-15 ) ) ;
#549=CARTESIAN_POINT ( 'NONE',  ( 1.447884101293554382, 9.556368569776049426, -0.5428950306860281794 ) ) ;
#561=CARTESIAN_POINT ( 'NONE',  ( -6.000000000000000888, 7.347880794884120722E-16, -12.00000000000000000 ) ) ;
#563=EDGE_CURVE ( 'NONE', #3747, #5361, #2873, .T. ) ;
#567=ORIENTED_EDGE ( 'NONE', *, *, #1362, .T. ) ;
#575=AXIS2_PLACEMENT_3D ( 'NONE', #2584, #3757, #4233 ) ;
#578=LINE ( 'NONE', #4762, #3087 ) ;
#597=PLANE ( 'NONE',  #2591 ) ;
#601=VERTEX_POINT ( 'NONE', #2623 ) ;
#604=CARTESIAN_POINT ( 'NONE',  ( 0.000000000000000000, 0.000000000000000000, -11.97459999999999880 ) ) ;
#606=CARTESIAN_POINT ( 'NONE',  ( 9.000000000000000000, -5.677101382972238319, -9.021433019664915065 ) ) ;
#613=EDGE_LOOP ( 'NONE', ( #1737, #3788, #3192, #3312 ) ) ;
#614=CARTESIAN_POINT ( 'NONE',  ( -9.497968775322179980, -4.580952057516538112, -9.518120616476199558 ) ) ;
#618=ADVANCED_FACE ( 'NONE', ( #2787 ), #1458, .T. ) ;
#619=ORIENTED_EDGE ( 'NONE', *, *, #1469, .F. ) ;
#620=CARTESIAN_POINT ( 'NONE',  ( 9.000000000000000000, 5.196152422706629359, -12.00000000000000000 ) ) ;
#622=CARTESIAN_POINT ( 'NONE',  ( 0.000000000000000000, 0.000000000000000000, -25.03750572909317285 ) ) ;
#626=CARTESIAN_POINT ( 'NONE',  ( 9.000000000000001776, -4.785828667975444262, -1.023175036954118378 ) ) ;
#627=CARTESIAN_POINT ( 'NONE',  ( -9.506737344437272696, -5.488717364925931541, -9.686084310752812954 ) ) ;
#628=CARTESIAN_POINT ( 'NONE',  ( 6.000000000000000000, 7.347880794884119736E-16, -11.97459999999999880 ) ) ;
#633=CARTESIAN_POINT ( 'NONE',  ( 9.000000000000000000, 0.9268837573866910429, -8.460786308154190749 ) ) ;
#638=DIRECTION ( 'NONE',  ( 0.000000000000000000, 0.000000000000000000, 1.000000000000000000 ) ) ;
#642=( BOUNDED_SURFACE ( )  B_SPLINE_SURFACE ( 3, 2, ( 
 ( #3137, #4384, #3580 ),
 ( #2317, #3990, #1119 ),
 ( #1173, #244, #1950 ),
 ( #3642, #3607, #2788 ),
 ( #3194, #2348, #2848 ),
 ( #1459, #3695, #4812 ),
 ( #4046, #1144, #2014 ),
 ( #5236, #2374, #712 ) ),
 .UNSPECIFIED., .F., .F., .T. ) 
 B_SPLINE_SURFACE_WITH_KNOTS ( ( 4, 2, 2, 4 ),
 ( 3, 3 ),
 ( 0.04613854442509286724, 0.05169925677048781143, 0.05447961294318528352, 0.05725996911588275562 ),
 ( 0.000000000000000000, 1.000000000000000000 ),
 .UNSPECIFIED. ) 
 GEOMETRIC_REPRESENTATION_ITEM ( )  RATIONAL_B_SPLINE_SURFACE ( (
 ( 1.000000000000000000, 0.8047781684971936356, 1.000000000000000000),
 ( 1.000000000000000000, 0.8123765127741280345, 1.000000000000000000),
 ( 1.000000000000000000, 0.8190661184402779904, 1.000000000000000000),
 ( 1.000000000000000000, 0.8191936944251213548, 1.000000000000000000),
 ( 1.000000000000000000, 0.8176092056339585579, 1.000000000000000000),
 ( 1.000000000000000000, 0.8122961334886904528, 1.000000000000000000),
 ( 1.000000000000000000, 0.8086310951057483765, 1.000000000000000000),
 ( 1.000000000000000000, 0.8047712311394934481, 1.000000000000000000) ) ) 
 REPRESENTATION_ITEM ( '' )  SURFACE ( )  );
#647=CARTESIAN_POINT ( 'NONE',  ( 6.048361762532168839, 6.900281553659078249, -0.1192015822679150933 ) ) ;
#648=DIRECTION ( 'NONE',  ( -0.000000000000000000, -0.000000000000000000, 1.000000000000000000 ) ) ;
#655=CARTESIAN_POINT ( 'NONE',  ( -1.301042606982605321E-14, -10.39230484541326760, -1.199999999999999734 ) ) ;
#657=DIRECTION ( 'NONE',  ( 1.000000000000000000, 0.000000000000000000, 0.000000000000000000 ) ) ;
#658=CARTESIAN_POINT ( 'NONE',  ( -8.716942385998455833, 5.934590066575458955, -9.518277236634762772 ) ) ;
#660=CARTESIAN_POINT ( 'NONE',  ( 0.000000000000000000, 0.000000000000000000, 0.000000000000000000 ) ) ;
#663=VECTOR ( 'NONE', #4725, 1000.000000000000000 ) ;
#666=CARTESIAN_POINT ( 'NONE',  ( 9.473646573774082924, 0.9034019355243676497, -9.137364994939673579 ) ) ;
#667=CARTESIAN_POINT ( 'NONE',  ( 5.999999999999999112, 6.928203230275508773, -8.505011083697292307 ) ) ;
#668=EDGE_LOOP ( 'NONE', ( #567, #1976, #3304, #3651 ) ) ;
#683=CARTESIAN_POINT ( 'NONE',  ( -5.284395884496540852, 7.341357458994635543, -0.03002505116509866095 ) ) ;
#689=B_SPLINE_CURVE_WITH_KNOTS ( 'NONE', 3,
 ( #2117, #2522, #1324, #4180, #4962, #1234, #1636, #5020 ),
 .UNSPECIFIED., .F., .F.,
 ( 4, 2, 2, 4 ),
 ( 0.007274027330054944063, 0.008608952725826013452, 0.009943878121597079373, 0.01261372891313921468 ),
 .UNSPECIFIED. ) ;
#690=ORIENTED_EDGE ( 'NONE', *, *, #3366, .F. ) ;
#692=PLANE ( 'NONE',  #3442 ) ;
#697=CARTESIAN_POINT ( 'NONE',  ( -0.7500000000000000000, -9.959292143521052409, -8.787392856021027043 ) ) ;
#700=DIRECTION ( 'NONE',  ( 0.000000000000000000, 0.000000000000000000, 1.000000000000000000 ) ) ;
#702=ORIENTED_EDGE ( 'NONE', *, *, #3214, .T. ) ;
#708=EDGE_CURVE ( 'NONE', #1655, #5213, #1163, .T. ) ;
#711=CARTESIAN_POINT ( 'NONE',  ( -9.000000000000007105, 5.196152422706624918, -9.106320693283315393 ) ) ;
#712=CARTESIAN_POINT ( 'NONE',  ( 0.05670911061056406466, -11.01091124578874414, -9.698321917585793983 ) ) ;
#713=CARTESIAN_POINT ( 'NONE',  ( 9.477403599784569366, 1.836490901034003809, -9.189746347754448763 ) ) ;
#723=B_SPLINE_CURVE_WITH_KNOTS ( 'NONE', 3,
 ( #4029, #2769, #5306, #277, #221, #1521, #4001, #4366, #3121, #627 ),
 .UNSPECIFIED., .F., .F.,
 ( 4, 2, 2, 2, 4 ),
 ( 1.620725098399643580E-19, 0.002766603965071790135, 0.005533207930143580269, 0.008299811895215371271, 0.01106641586028715880 ),
 .UNSPECIFIED. ) ;
#728=EDGE_CURVE ( 'NONE', #3383, #2814, #2200, .T. ) ;
#737=EDGE_CURVE ( 'NONE', #4965, #428, #3178, .T. ) ;
#745=VERTEX_POINT ( 'NONE', #1900 ) ;
#754=VERTEX_POINT ( 'NONE', #268 ) ;
#762=EDGE_CURVE ( 'NONE', #1094, #3611, #3337, .T. ) ;
#769=DIRECTION ( 'NONE',  ( 1.000000000000000000, 0.000000000000000000, 0.000000000000000000 ) ) ;
#783=CARTESIAN_POINT ( 'NONE',  ( 0.000000000000000000, -10.39230484541327293, -8.935996291721338025 ) ) ;
#789=DIRECTION ( 'NONE',  ( 0.5000000000000004441, -0.8660254037844384856, 0.000000000000000000 ) ) ;
#790=CARTESIAN_POINT ( 'NONE',  ( -0.7500000000000007772, 9.959292143521045304, -8.787392856021023491 ) ) ;
#793=FACE_OUTER_BOUND ( 'NONE', #4731, .T. ) ;
#795=ORIENTED_EDGE ( 'NONE', *, *, #3460, .F. ) ;
#798=CARTESIAN_POINT ( 'NONE',  ( -1.499235438992549296, 10.09238013696277037, -9.361164777501199907 ) ) ;
#810=ORIENTED_EDGE ( 'NONE', *, *, #233, .F. ) ;
#811=LINE ( 'NONE', #4169, #51 ) ;
#815=ORIENTED_EDGE ( 'NONE', *, *, #4633, .T. ) ;
#818=CYLINDRICAL_SURFACE ( 'NONE', #2939, 5.099999999999999645 ) ;
#822=CARTESIAN_POINT ( 'NONE',  ( -8.758033615148283602, 5.911365213026127385, -9.525564194215435876 ) ) ;
#824=CARTESIAN_POINT ( 'NONE',  ( 7.950863337915118123, -6.367515845290791177, -9.383905213721023486 ) ) ;
#832=CIRCLE ( 'NONE', #2303, 9.000000000000001776 ) ;
#853=CARTESIAN_POINT ( 'NONE',  ( -2.790577774332636096, 8.781164016207728906, -8.465119797812908686 ) ) ;
#856=DIRECTION ( 'NONE',  ( -1.000000000000000000, 0.000000000000000000, 0.000000000000000000 ) ) ;
#857=VECTOR ( 'NONE', #2717, 1000.000000000000000 ) ;
#860=CARTESIAN_POINT ( 'NONE',  ( -9.507358266631047883, 5.552911536195821895, -9.698012930120947672 ) ) ;
#865=CARTESIAN_POINT ( 'NONE',  ( 2.893723230124677137, 8.721612959541547028, -9.019248292997474437 ) ) ;
#867=ORIENTED_EDGE ( 'NONE', *, *, #4375, .F. ) ;
#880=CARTESIAN_POINT ( 'NONE',  ( 0.000000000000000000, 0.000000000000000000, -10.20000000000000107 ) ) ;
#885=CARTESIAN_POINT ( 'NONE',  ( 9.000000000000001776, 4.367518130255698239, -0.8586158810094328686 ) ) ;
#887=CARTESIAN_POINT ( 'NONE',  ( 7.552115898706448505, -6.032088698343846644, -0.5428950306860315100 ) ) ;
#892=CARTESIAN_POINT ( 'NONE',  ( 5.303004762135293149, -7.330613618480590787, -8.460795847314498630 ) ) ;
#893=B_SPLINE_CURVE_WITH_KNOTS ( 'NONE', 3,
 ( #3621, #3684, #1159, #1269, #1583, #1133, #2801, #3661, #3266 ),
 .UNSPECIFIED., .F., .F.,
 ( 4, 2, 1, 2, 4 ),
 ( 0.000000000000000000, 0.002598076211353316303, 0.005196152422706632606, 0.007794228634059949777, 0.01039230484541326521 ),
 .UNSPECIFIED. ) ;
#895=CARTESIAN_POINT ( 'NONE',  ( -5.010000000000002451, 6.135480463728242006E-16, -0.6932054628276118624 ) ) ;
#898=CARTESIAN_POINT ( 'NONE',  ( 5.099999999999999645, 0.000000000000000000, -11.34441321561125626 ) ) ;
#899=CARTESIAN_POINT ( 'NONE',  ( -9.000000000000000000, -5.678788000576118655, -9.021742658504674495 ) ) ;
#905=CARTESIAN_POINT ( 'NONE',  ( 9.000000000000000000, 5.196152422706636465, -1.199999999999999734 ) ) ;
#915=CARTESIAN_POINT ( 'NONE',  ( 2.999999999999998668, 8.660254037844387298, -8.505011083697294083 ) ) ;
#920=AXIS2_PLACEMENT_3D ( 'NONE', #2464, #4463, #2817 ) ;
#922=CARTESIAN_POINT ( 'NONE',  ( -8.999999999999998224, 3.519160108721328228, -0.5651793076691160600 ) ) ;
#923=CARTESIAN_POINT ( 'NONE',  ( 9.477420239195661011, -1.840077440320891045, -9.189982433786857641 ) ) ;
#924=DIRECTION ( 'NONE',  ( 1.000000000000000000, 0.000000000000000000, 0.000000000000000000 ) ) ;
#929=( NAMED_UNIT ( * ) SI_UNIT ( $, .STERADIAN. ) SOLID_ANGLE_UNIT ( ) );
#932=VERTEX_POINT ( 'NONE', #3393 ) ;
#937=EDGE_CURVE ( 'NONE', #4400, #601, #5166, .T. ) ;
#946=CARTESIAN_POINT ( 'NONE',  ( -9.000000000000001776, 0.000000000000000000, 0.000000000000000000 ) ) ;
#949=DIRECTION ( 'NONE',  ( -1.000000000000000000, 0.000000000000000000, 0.000000000000000000 ) ) ;
#951=FILL_AREA_STYLE_COLOUR ( '', #1708 ) ;
#957=CARTESIAN_POINT ( 'NONE',  ( 9.000000000000000000, 5.196152422706636465, -1.199999999999999734 ) ) ;
#967=CARTESIAN_POINT ( 'NONE',  ( -9.477420239195661011, 1.840077440320891711, -9.189982433786857641 ) ) ;
#970=DIRECTION ( 'NONE',  ( -0.000000000000000000, -0.000000000000000000, 1.000000000000000000 ) ) ;
#973=CARTESIAN_POINT ( 'NONE',  ( 9.000000000000000000, -5.196152422706636465, -12.00000000000000000 ) ) ;
#976=PRODUCT ( 'hex flange nut gradea_iso_ISO - 4161 - M12 - N', 'hex flange nut gradea_iso_ISO - 4161 - M12 - N', '', ( #5267 ) ) ;
#980=CARTESIAN_POINT ( 'NONE',  ( 9.000000000000003553, -1.784038208492157551, -0.1183376658062880588 ) ) ;
#982=ORIENTED_EDGE ( 'NONE', *, *, #1792, .F. ) ;
#1002=ORIENTED_EDGE ( 'NONE', *, *, #3242, .T. ) ;
#1014=ADVANCED_FACE ( 'NONE', ( #3469 ), #5085, .T. ) ;
#1020=FACE_OUTER_BOUND ( 'NONE', #1227, .T. ) ;
#1022=AXIS2_PLACEMENT_3D ( 'NONE', #2060, #3741, #3211 ) ;
#1026=VECTOR ( 'NONE', #700, 1000.000000000000000 ) ;
#1046=CARTESIAN_POINT ( 'NONE',  ( 2.951638237467836046, -8.688175714460822263, -0.1192015822679215187 ) ) ;
#1050=CARTESIAN_POINT ( 'NONE',  ( 9.000000000000000000, 3.792226493019370093, -8.707316330048348263 ) ) ;
#1055=DIRECTION ( 'NONE',  ( -1.000000000000000000, 0.000000000000000000, 0.000000000000000000 ) ) ;
#1071=CIRCLE ( 'NONE', #4136, 6.000000000000000888 ) ;
#1072=( BOUNDED_SURFACE ( )  B_SPLINE_SURFACE ( 3, 2, ( 
 ( #2463, #2544, #1714 ),
 ( #4520, #2569, #798 ),
 ( #853, #2072, #1633 ),
 ( #56, #490, #1597 ),
 ( #460, #5045, #4127 ),
 ( #3727, #3773, #3752 ),
 ( #3283, #3338, #822 ),
 ( #4988, #5348, #2149 ) ),
 .UNSPECIFIED., .F., .F., .T. ) 
 B_SPLINE_SURFACE_WITH_KNOTS ( ( 4, 2, 2, 4 ),
 ( 3, 3 ),
 ( 0.04613854442509285336, 0.05169925677048779755, 0.05447961294318526965, 0.05725996911588274174 ),
 ( 0.000000000000000000, 1.000000000000000000 ),
 .UNSPECIFIED. ) 
 GEOMETRIC_REPRESENTATION_ITEM ( )  RATIONAL_B_SPLINE_SURFACE ( (
 ( 1.000000000000000000, 0.8047781684971931915, 1.000000000000000000),
 ( 1.000000000000000000, 0.8123765127742886838, 1.000000000000000000),
 ( 1.000000000000000000, 0.8190661184400637174, 1.000000000000000000),
 ( 1.000000000000000000, 0.8191936944252291575, 1.000000000000000000),
 ( 1.000000000000000000, 0.8176092056337987968, 1.000000000000000000),
 ( 1.000000000000000000, 0.8122961334888495477, 1.000000000000000000),
 ( 1.000000000000000000, 0.8086310951056294716, 1.000000000000000000),
 ( 1.000000000000000000, 0.8047712311394933371, 1.000000000000000000) ) ) 
 REPRESENTATION_ITEM ( '' )  SURFACE ( )  );
#1079=ORIENTED_EDGE ( 'NONE', *, *, #1395, .T. ) ;
#1084=CIRCLE ( 'NONE', #4472, 0.9279820837131848021 ) ;
#1094=VERTEX_POINT ( 'NONE', #1114 ) ;
#1100=CARTESIAN_POINT ( 'NONE',  ( -9.000000000000000000, -5.196152422706635576, -9.106320693283315393 ) ) ;
#1104=FACE_OUTER_BOUND ( 'NONE', #5003, .T. ) ;
#1114=CARTESIAN_POINT ( 'NONE',  ( -9.473745496805529243, -1.478735707944909295E-13, -9.138786188337405747 ) ) ;
#1115=CARTESIAN_POINT ( 'NONE',  ( 0.000000000000000000, 0.000000000000000000, -12.00000000000000000 ) ) ;
#1119=CARTESIAN_POINT ( 'NONE',  ( -7.990639863761101580, -6.344566044901012170, -9.361164777500285084 ) ) ;
#1120=CARTESIAN_POINT ( 'NONE',  ( 9.489595936502764673, 3.666866907830382161, -9.379652974972602308 ) ) ;
#1131=AXIS2_PLACEMENT_3D ( 'NONE', #251, #4391, #657 ) ;
#1133=CARTESIAN_POINT ( 'NONE',  ( 9.000000000000000000, 1.732050807568874529, -8.505011083697297636 ) ) ;
#1139=B_SPLINE_CURVE_WITH_KNOTS ( 'NONE', 3,
 ( #166, #214, #4700, #4679, #3959, #4310 ),
 .UNSPECIFIED., .F., .F.,
 ( 4, 2, 4 ),
 ( 0.000000000000000000, 0.0005027859236379887426, 0.001005571847275977485 ),
 .UNSPECIFIED. ) ;
#1141=ORIENTED_EDGE ( 'NONE', *, *, #3126, .T. ) ;
#1144=CARTESIAN_POINT ( 'NONE',  ( -0.4650146599150260518, -10.12382850633293430, -9.367146555587614998 ) ) ;
#1159=CARTESIAN_POINT ( 'NONE',  ( 9.000000000000000000, -3.464101615137758383, -8.667800885990210702 ) ) ;
#1161=ORIENTED_EDGE ( 'NONE', *, *, #5139, .T. ) ;
#1162=EDGE_LOOP ( 'NONE', ( #5302, #1244, #3693 ) ) ;
#1163=B_SPLINE_CURVE_WITH_KNOTS ( 'NONE', 3,
 ( #209, #4811, #5177, #3579, #711, #2347 ),
 .UNSPECIFIED., .F., .F.,
 ( 4, 2, 4 ),
 ( -5.636559625666591986E-06, 0.0004989239064927796776, 0.001003484372611225962 ),
 .UNSPECIFIED. ) ;
#1164=ORIENTED_EDGE ( 'NONE', *, *, #5118, .T. ) ;
#1170=AXIS2_PLACEMENT_3D ( 'NONE', #1540, #292, #4434 ) ;
#1173=CARTESIAN_POINT ( 'NONE',  ( -6.209422225667362127, -6.807293251912172494, -8.465119797811233582 ) ) ;
#1177=EDGE_CURVE ( 'NONE', #3466, #2814, #2395, .T. ) ;
#1183=CARTESIAN_POINT ( 'NONE',  ( -9.000000000000000000, -5.196152422706636465, -8.935996291721336249 ) ) ;
#1188=CONICAL_SURFACE ( 'NONE', #1866, 12.38940648156203927, 1.221730476396048370 ) ;
#1197=CIRCLE ( 'NONE', #920, 9.000000000000001776 ) ;
#1214=ORIENTED_EDGE ( 'NONE', *, *, #2467, .F. ) ;
#1217=CARTESIAN_POINT ( 'NONE',  ( 0.000000000000000000, 0.000000000000000000, -12.00000000000000178 ) ) ;
#1219=CARTESIAN_POINT ( 'NONE',  ( 3.936978610624179531, 8.666338374798533195, -9.138972935415379695 ) ) ;
#1220=ORIENTED_EDGE ( 'NONE', *, *, #1722, .F. ) ;
#1221=ORIENTED_EDGE ( 'NONE', *, *, #328, .T. ) ;
#1222=CARTESIAN_POINT ( 'NONE',  ( 9.506737344437272696, 5.488717364925924436, -9.686084310752812954 ) ) ;
#1225=VERTEX_POINT ( 'NONE', #1421 ) ;
#1227=EDGE_LOOP ( 'NONE', ( #3360, #5032, #123 ) ) ;
#1230=ORIENTED_EDGE ( 'NONE', *, *, #2338, .F. ) ;
#1234=CARTESIAN_POINT ( 'NONE',  ( -9.000000000000003553, -1.784038208492157329, -0.1183376658062878922 ) ) ;
#1240=CARTESIAN_POINT ( 'NONE',  ( -9.000000000000000000, 3.843049336495677260, -8.684764317652872379 ) ) ;
#1244=ORIENTED_EDGE ( 'NONE', *, *, #937, .F. ) ;
#1245=ORIENTED_EDGE ( 'NONE', *, *, #4608, .T. ) ;
#1252=CARTESIAN_POINT ( 'NONE',  ( -0.05527946870650939093, -11.01006727514132066, -9.698012095152312995 ) ) ;
#1263=ORIENTED_EDGE ( 'NONE', *, *, #3700, .T. ) ;
#1264=CARTESIAN_POINT ( 'NONE',  ( 9.000000000000000000, 5.196152422706629359, -12.00000000000000000 ) ) ;
#1269=CARTESIAN_POINT ( 'NONE',  ( 8.999999999999998224, -1.732050807568880968, -8.505011083697294083 ) ) ;
#1272=ADVANCED_FACE ( 'NONE', ( #4042 ), #3632, .T. ) ;
#1278=VECTOR ( 'NONE', #1829, 1000.000000000000000 ) ;
#1281=CARTESIAN_POINT ( 'NONE',  ( 9.000000000000001776, -5.196152422706638241, -1.199999999999999734 ) ) ;
#1284=DIRECTION ( 'NONE',  ( 1.000000000000000000, 0.000000000000000000, -0.000000000000000000 ) ) ;
#1287=CARTESIAN_POINT ( 'NONE',  ( -3.715604115503467142, -8.247099809125261416, -0.03002505116510541944 ) ) ;
#1290=CARTESIAN_POINT ( 'NONE',  ( -8.999999999999998224, 1.936561697304590934, -8.969347964766754444 ) ) ;
#1295=CARTESIAN_POINT ( 'NONE',  ( 0.4650146599169583395, 10.12382850633530751, -9.367146555589735968 ) ) ;
#1296=CARTESIAN_POINT ( 'NONE',  ( 6.332118058842089781, -7.287734290476359789, -9.190020220263406259 ) ) ;
#1297=ORIENTED_EDGE ( 'NONE', *, *, #2518, .F. ) ;
#1298=ORIENTED_EDGE ( 'NONE', *, *, #4429, .T. ) ;
#1305=DIRECTION ( 'NONE',  ( 1.000000000000000000, 0.000000000000000000, 0.000000000000000000 ) ) ;
#1306=CARTESIAN_POINT ( 'NONE',  ( -9.000000000000000000, 1.123146974283612654, -0.05788585198792847025 ) ) ;
#1309=CARTESIAN_POINT ( 'NONE',  ( -2.569563281917990771, -8.908766792898138220, -0.2264046624879807734 ) ) ;
#1311=CARTESIAN_POINT ( 'NONE',  ( -9.473946373357962969, 1.923623857792322145, -9.141672110797713913 ) ) ;
#1315=ADVANCED_FACE ( 'NONE', ( #4622, #2153 ), #438, .T. ) ;
#1324=CARTESIAN_POINT ( 'NONE',  ( -9.000000000000000000, -4.368650009232622367, -0.8589767385557532942 ) ) ;
#1327=CARTESIAN_POINT ( 'NONE',  ( 9.473745496805529243, 1.478328004173170497E-13, -9.138786188337405747 ) ) ;
#1332=CARTESIAN_POINT ( 'NONE',  ( -9.000000000000000000, -4.737975421414065913, -8.849003814629385900 ) ) ;
#1335=ORIENTED_EDGE ( 'NONE', *, *, #2449, .T. ) ;
#1337=CARTESIAN_POINT ( 'NONE',  ( 3.145560420647533828, 9.127459525684209041, -9.189462574975609144 ) ) ;
#1341=EDGE_CURVE ( 'NONE', #3771, #2114, #4674, .T. ) ;
#1342=CARTESIAN_POINT ( 'NONE',  ( -5.099999999999999645, 6.245698675651500839E-16, -12.00000000000000000 ) ) ;
#1344=AXIS2_PLACEMENT_3D ( 'NONE', #3711, #3210, #3301 ) ;
#1346=ORIENTED_EDGE ( 'NONE', *, *, #2543, .F. ) ;
#1350=ORIENTED_EDGE ( 'NONE', *, *, #391, .F. ) ;
#1351=DIRECTION ( 'NONE',  ( 0.000000000000000000, 0.000000000000000000, -1.000000000000000000 ) ) ;
#1362=EDGE_CURVE ( 'NONE', #3765, #754, #3791, .T. ) ;
#1363=ADVANCED_FACE ( 'NONE', ( #3441 ), #383, .F. ) ;
#1367=CARTESIAN_POINT ( 'NONE',  ( 6.209422225666635597, 6.807293251912587273, -8.465119797812908686 ) ) ;
#1382=CARTESIAN_POINT ( 'NONE',  ( 0.7169666604817516165, -9.978363950984148190, -0.8432325327665534109 ) ) ;
#1390=B_SPLINE_CURVE_WITH_KNOTS ( 'NONE', 3,
 ( #2023, #2420, #1579, #1556, #1219, #3261, #2448, #2472, #2859, #4089 ),
 .UNSPECIFIED., .F., .F.,
 ( 4, 2, 2, 2, 4 ),
 ( 0.000000000000000000, 0.002766603965071789701, 0.005533207930143578535, 0.008299811895215367802, 0.01106641586028715707 ),
 .UNSPECIFIED. ) ;
#1395=EDGE_CURVE ( 'NONE', #4086, #3383, #4755, .T. ) ;
#1408=EDGE_CURVE ( 'NONE', #4400, #1225, #4074, .T. ) ;
#1412=CARTESIAN_POINT ( 'NONE',  ( 9.000000000000000000, 5.196152422706629359, -8.935996291721334472 ) ) ;
#1421=CARTESIAN_POINT ( 'NONE',  ( -1.301042606982605321E-14, -10.39230484541326760, -1.199999999999999734 ) ) ;
#1424=B_SPLINE_CURVE_WITH_KNOTS ( 'NONE', 3,
 ( #4412, #4873, #647, #4439, #3250, #1513 ),
 .UNSPECIFIED., .F., .F.,
 ( 4, 2, 4 ),
 ( 0.005333245961717302495, 0.007986067645924079320, 0.01063888933013085701 ),
 .UNSPECIFIED. ) ;
#1427=EDGE_LOOP ( 'NONE', ( #1220, #3769, #1141, #1214 ) ) ;
#1430=CARTESIAN_POINT ( 'NONE',  ( -9.000000000000000000, 5.196152422706629359, -1.199999999999997291 ) ) ;
#1435=CIRCLE ( 'NONE', #4240, 0.9279820837131848021 ) ;
#1439=CARTESIAN_POINT ( 'NONE',  ( -9.000000000000000000, 5.196152422706629359, -12.00000000000000000 ) ) ;
#1442=DIRECTION ( 'NONE',  ( 0.000000000000000000, 0.000000000000000000, -1.000000000000000000 ) ) ;
#1443=B_SPLINE_CURVE_WITH_KNOTS ( 'NONE', 3,
 ( #1412, #4742, #425, #4451, #4914, #1222 ),
 .UNSPECIFIED., .F., .F.,
 ( 4, 2, 4 ),
 ( 1.734723475976807094E-18, 0.0005027859236379904773, 0.001005571847275979220 ),
 .UNSPECIFIED. ) ;
#1451=CARTESIAN_POINT ( 'NONE',  ( 0.000000000000000000, 0.000000000000000000, 0.000000000000000000 ) ) ;
#1455=ADVANCED_FACE ( 'NONE', ( #1803 ), #4560, .T. ) ;
#1458=PLANE ( 'NONE',  #4051 ) ;
#1459=CARTESIAN_POINT ( 'NONE',  ( -1.215778977584765608, -9.690374525429620078, -8.707326526324040472 ) ) ;
#1469=EDGE_CURVE ( 'NONE', #3920, #601, #2517, .T. ) ;
#1470=CARTESIAN_POINT ( 'NONE',  ( 8.999999999999998224, -1.936944919200365156, -8.969396369466336338 ) ) ;
#1471=DIRECTION ( 'NONE',  ( 1.000000000000000000, 0.000000000000000000, 0.000000000000000000 ) ) ;
#1474=ORIENTED_EDGE ( 'NONE', *, *, #2136, .F. ) ;
#1477=CARTESIAN_POINT ( 'NONE',  ( -5.099999999999999645, 6.245698675651500839E-16, -11.34441321561125626 ) ) ;
#1481=EDGE_CURVE ( 'NONE', #5234, #1794, #578, .T. ) ;
#1490=ORIENTED_EDGE ( 'NONE', *, *, #4897, .F. ) ;
#1492=FACE_OUTER_BOUND ( 'NONE', #346, .T. ) ;
#1494=CARTESIAN_POINT ( 'NONE',  ( 9.000000000000000000, 5.196152422706629359, -12.00000000000000000 ) ) ;
#1506=ORIENTED_EDGE ( 'NONE', *, *, #1408, .T. ) ;
#1513=CARTESIAN_POINT ( 'NONE',  ( 9.000000000000000000, 5.196152422706636465, -1.199999999999999734 ) ) ;
#1515=CARTESIAN_POINT ( 'NONE',  ( -9.506737344437272696, -5.488717364925931541, -9.686084310752812954 ) ) ;
#1521=CARTESIAN_POINT ( 'NONE',  ( -5.527857873577812775, -7.747813868291107298, -9.138600484129264956 ) ) ;
#1524=CARTESIAN_POINT ( 'NONE',  ( -9.506737344437272696, -5.488717364925931541, -9.686084310752812954 ) ) ;
#1526=B_SPLINE_CURVE_WITH_KNOTS ( 'NONE', 3,
 ( #1692, #4265, #4186, #4164, #422, #17, #2554, #1668, #3344 ),
 .UNSPECIFIED., .F., .F.,
 ( 4, 2, 1, 2, 4 ),
 ( 0.000000000000000000, 0.002598076211353316737, 0.005196152422706633474, 0.007794228634059948910, 0.01039230484541326521 ),
 .UNSPECIFIED. ) ;
#1539=ORIENTED_EDGE ( 'NONE', *, *, #3610, .T. ) ;
#1540=CARTESIAN_POINT ( 'NONE',  ( -2.352990130084610634E-16, 10.39230484541326582, -12.00000000000000000 ) ) ;
#1545=FACE_OUTER_BOUND ( 'NONE', #1662, .T. ) ;
#1556=CARTESIAN_POINT ( 'NONE',  ( 3.145304002162439438, 9.127642243957637902, -9.190020220263409811 ) ) ;
#1566=ORIENTED_EDGE ( 'NONE', *, *, #328, .F. ) ;
#1579=CARTESIAN_POINT ( 'NONE',  ( 1.567730871772294865, 10.05252977580646068, -9.379910571084325355 ) ) ;
#1583=CARTESIAN_POINT ( 'NONE',  ( 9.000000000000000000, -2.602085213965210247E-15, -8.419403919045800322 ) ) ;
#1589=EDGE_LOOP ( 'NONE', ( #4340, #2538, #1674, #2334, #2680, #3027 ) ) ;
#1593=AXIS2_PLACEMENT_3D ( 'NONE', #5073, #970, #2548 ) ;
#1597=CARTESIAN_POINT ( 'NONE',  ( -5.519484922003735861, 7.752549460314756224, -9.137374534098906764 ) ) ;
#1604=CARTESIAN_POINT ( 'NONE',  ( -8.038218111920156501E-16, -10.97743472985186486, -9.686084310752816506 ) ) ;
#1606=FACE_OUTER_BOUND ( 'NONE', #1427, .T. ) ;
#1611=ORIENTED_EDGE ( 'NONE', *, *, #2928, .T. ) ;
#1613=CARTESIAN_POINT ( 'NONE',  ( -8.250000000000000000, 5.629165124598848990, -8.787392856021023491 ) ) ;
#1615=ADVANCED_BREP_SHAPE_REPRESENTATION ( '', ( #3657, #4154 ), #315 ) ;
#1617=ADVANCED_FACE ( 'NONE', ( #1492 ), #692, .T. ) ;
#1621=ORIENTED_EDGE ( 'NONE', *, *, #4781, .T. ) ;
#1624=CIRCLE ( 'NONE', #2771, 6.000000000000000000 ) ;
#1633=CARTESIAN_POINT ( 'NONE',  ( -3.070858717647508396, 9.166611990351359651, -9.141698485139983177 ) ) ;
#1634=SHAPE_REPRESENTATION ( 'hex flange nut gradea_iso_ISO - 4161 - M12 - N', ( #4154 ), #315 ) ;
#1636=CARTESIAN_POINT ( 'NONE',  ( -9.000000000000000000, -0.9015406389697722123, 1.312336379612662396E-15 ) ) ;
#1642=CARTESIAN_POINT ( 'NONE',  ( 8.327614167581914066E-17, -10.39230484541327115, -9.106324069981644342 ) ) ;
#1650=EDGE_LOOP ( 'NONE', ( #3412, #1621, #4704, #1985, #1506 ) ) ;
#1655=VERTEX_POINT ( 'NONE', #5329 ) ;
#1656=ORIENTED_EDGE ( 'NONE', *, *, #2518, .T. ) ;
#1659=FACE_OUTER_BOUND ( 'NONE', #534, .T. ) ;
#1660=CARTESIAN_POINT ( 'NONE',  ( 6.134460314789567548, -6.850572531336434068, -8.512883888440004654 ) ) ;
#1662=EDGE_LOOP ( 'NONE', ( #4437, #810, #4037, #1804 ) ) ;
#1667=EDGE_CURVE ( 'NONE', #5291, #1919, #2890, .T. ) ;
#1668=CARTESIAN_POINT ( 'NONE',  ( 8.250000000000000000, -5.629165124598856984, -8.787392856021023491 ) ) ;
#1672=CARTESIAN_POINT ( 'NONE',  ( 3.712196824332475220, 8.249067009600011602, -8.964894084809515107 ) ) ;
#1674=ORIENTED_EDGE ( 'NONE', *, *, #1177, .T. ) ;
#1680=ORIENTED_EDGE ( 'NONE', *, *, #3610, .F. ) ;
#1691=CARTESIAN_POINT ( 'NONE',  ( -4.500000000000003553, 7.794228634059947147, 0.000000000000000000 ) ) ;
#1692=CARTESIAN_POINT ( 'NONE',  ( 0.000000000000000000, -10.39230484541327293, -8.935996291721338025 ) ) ;
#1694=CIRCLE ( 'NONE', #3014, 6.000000000000000000 ) ;
#1696=DIRECTION ( 'NONE',  ( -0.000000000000000000, -0.000000000000000000, 1.000000000000000000 ) ) ;
#1708=COLOUR_RGB ( '',1.000000000000000000, 0.9490196078431372140, 0.9098039215686274384 ) ;
#1714=CARTESIAN_POINT ( 'NONE',  ( 0.05527946870651088973, 11.01006727514131356, -9.698012095152311218 ) ) ;
#1717=AXIS2_PLACEMENT_3D ( 'NONE', #3591, #1442, #2693 ) ;
#1722=EDGE_CURVE ( 'NONE', #754, #3611, #1084, .T. ) ;
#1723=AXIS2_PLACEMENT_3D ( 'NONE', #2570, #2937, #1305 ) ;
#1724=CARTESIAN_POINT ( 'NONE',  ( -1.453914506656639238, 9.552886913616349673, -0.5405968996908959712 ) ) ;
#1726=CARTESIAN_POINT ( 'NONE',  ( -9.000000000001600498, 3.788414693531317656, -9.200428974772291824 ) ) ;
#1730=CARTESIAN_POINT ( 'NONE',  ( 7.828285197793313444, 5.872642279174128177, -8.684787165848931068 ) ) ;
#1737=ORIENTED_EDGE ( 'NONE', *, *, #3481, .F. ) ;
#1740=CARTESIAN_POINT ( 'NONE',  ( 0.000000000000000000, 0.000000000000000000, 0.000000000000000000 ) ) ;
#1741=CARTESIAN_POINT ( 'NONE',  ( 7.727639453308645656, -5.930750126846072945, -9.220334578152900917 ) ) ;
#1742=CARTESIAN_POINT ( 'NONE',  ( -9.000000000000000000, 3.091092034686353518, -0.4369508170668109925 ) ) ;
#1743=ORIENTED_EDGE ( 'NONE', *, *, #1341, .F. ) ;
#1745=( NAMED_UNIT ( * ) SI_UNIT ( $, .STERADIAN. ) SOLID_ANGLE_UNIT ( ) );
#1746=DIRECTION ( 'NONE',  ( 1.000000000000000000, 0.000000000000000000, 0.000000000000000000 ) ) ;
#1753=CARTESIAN_POINT ( 'NONE',  ( 1.215778977584813125, 9.690374525429584551, -8.707326526324868254 ) ) ;
#1754=CARTESIAN_POINT ( 'NONE',  ( 9.000000000000001776, 3.091092034686357071, -0.4369508170668111591 ) ) ;
#1755=EDGE_CURVE ( 'NONE', #1094, #1655, #2696, .T. ) ;
#1790=AXIS2_PLACEMENT_3D ( 'NONE', #1494, #3169, #5248 ) ;
#1792=EDGE_CURVE ( 'NONE', #601, #3466, #832, .T. ) ;
#1793=CARTESIAN_POINT ( 'NONE',  ( -9.000000000000000000, 5.196152422706629359, -1.199999999999997291 ) ) ;
#1794=VERTEX_POINT ( 'NONE', #3028 ) ;
#1797=CARTESIAN_POINT ( 'NONE',  ( -9.000000000000000000, 1.732050807568874085, -8.505011083697295859 ) ) ;
#1802=CONICAL_SURFACE ( 'NONE', #5299, 9.000000000000001776, 0.8594454914424796144 ) ;
#1803=FACE_OUTER_BOUND ( 'NONE', #668, .T. ) ;
#1804=ORIENTED_EDGE ( 'NONE', *, *, #4657, .F. ) ;
#1811=CARTESIAN_POINT ( 'NONE',  ( -6.000000000000000000, 7.347880794884119736E-16, 0.000000000000000000 ) ) ;
#1820=EDGE_LOOP ( 'NONE', ( #1346, #3792, #1335, #3477, #3130 ) ) ;
#1829=DIRECTION ( 'NONE',  ( 0.8191520442889915765, 0.000000000000000000, 0.5735764363510464925 ) ) ;
#1832=EDGE_CURVE ( 'NONE', #4959, #1094, #1967, .T. ) ;
#1835=CARTESIAN_POINT ( 'NONE',  ( 1.500000000000000666, 9.526279441628828337, -8.667800885990208926 ) ) ;
#1838=CARTESIAN_POINT ( 'NONE',  ( -9.477403599784569366, -1.836490901034005807, -9.189746347754448763 ) ) ;
#1843=LINE ( 'NONE', #973, #3737 ) ;
#1854=LINE ( 'NONE', #2302, #1026 ) ;
#1856=VERTEX_POINT ( 'NONE', #1477 ) ;
#1859=ORIENTED_EDGE ( 'NONE', *, *, #4409, .T. ) ;
#1864=DIRECTION ( 'NONE',  ( 1.000000000000000000, 0.000000000000000000, 0.000000000000000000 ) ) ;
#1865=CIRCLE ( 'NONE', #1344, 12.38940648156203927 ) ;
#1866=AXIS2_PLACEMENT_3D ( 'NONE', #3854, #542, #3138 ) ;
#1869=CARTESIAN_POINT ( 'NONE',  ( -2.352990130084610634E-16, 10.39230484541326582, -8.935996291721336249 ) ) ;
#1874=ADVANCED_FACE ( 'NONE', ( #4837 ), #4729, .T. ) ;
#1879=CARTESIAN_POINT ( 'NONE',  ( 8.999999999999998224, -3.516072269208508683, -0.5641419778896282766 ) ) ;
#1886=CARTESIAN_POINT ( 'NONE',  ( 9.000000000000000000, 1.854613033839518588, -9.019235192255276701 ) ) ;
#1889=ADVANCED_FACE ( 'NONE', ( #2751, #4406 ), #4374, .F. ) ;
#1892=CARTESIAN_POINT ( 'NONE',  ( -9.473745496805531019, -0.9193675319299582371, -9.138786188337409300 ) ) ;
#1893=ORIENTED_EDGE ( 'NONE', *, *, #4322, .F. ) ;
#1898=EDGE_CURVE ( 'NONE', #1919, #5042, #1694, .T. ) ;
#1900=CARTESIAN_POINT ( 'NONE',  ( 6.000000000000000888, 0.000000000000000000, -12.00000000000000000 ) ) ;
#1902=DIRECTION ( 'NONE',  ( 0.000000000000000000, 0.000000000000000000, 1.000000000000000000 ) ) ;
#1919=VERTEX_POINT ( 'NONE', #4924 ) ;
#1921=ORIENTED_EDGE ( 'NONE', *, *, #1667, .T. ) ;
#1928=ADVANCED_FACE ( 'NONE', ( #793 ), #818, .F. ) ;
#1935=CARTESIAN_POINT ( 'NONE',  ( 9.000000000000000000, -3.843229588189086776, -8.684797700342420157 ) ) ;
#1949=CARTESIAN_POINT ( 'NONE',  ( -6.052010058236153789, 6.898175209152294762, -0.1432599722965965938 ) ) ;
#1950=CARTESIAN_POINT ( 'NONE',  ( -6.403089491455932425, -7.242747656089419728, -9.141698485139452046 ) ) ;
#1962=ORIENTED_EDGE ( 'NONE', *, *, #4421, .F. ) ;
#1967=B_SPLINE_CURVE_WITH_KNOTS ( 'NONE', 3,
 ( #3601, #614, #5256, #1838, #1892, #3219 ),
 .UNSPECIFIED., .F., .F.,
 ( 4, 2, 4 ),
 ( 0.000000000000000000, 0.002769186132444451109, 0.005538372264888902219 ),
 .UNSPECIFIED. ) ;
#1970=( GEOMETRIC_REPRESENTATION_CONTEXT ( 3 ) GLOBAL_UNCERTAINTY_ASSIGNED_CONTEXT ( ( #4081 ) ) GLOBAL_UNIT_ASSIGNED_CONTEXT ( ( #4993, #3756, #1745 ) ) REPRESENTATION_CONTEXT ( 'NONE', 'WORKASPACE' ) );
#1975=AXIS2_PLACEMENT_3D ( 'NONE', #4462, #331, #4845 ) ;
#1976=ORIENTED_EDGE ( 'NONE', *, *, #1722, .T. ) ;
#1985=ORIENTED_EDGE ( 'NONE', *, *, #2144, .T. ) ;
#1989=CARTESIAN_POINT ( 'NONE',  ( -0.4165158504820766772, -10.63278038381084478, -9.021433408186455338 ) ) ;
#2002=PRODUCT_DEFINITION_CONTEXT ( 'detailed design', #3948, 'design' ) ;
#2013=DIRECTION ( 'NONE',  ( -0.9396926207859145341, 0.000000000000000000, -0.3420201433256521151 ) ) ;
#2014=CARTESIAN_POINT ( 'NONE',  ( -0.7403756379546261313, -10.54036220443003913, -9.525564194215615288 ) ) ;
#2023=CARTESIAN_POINT ( 'NONE',  ( 3.049442433610978414E-16, 10.97743472985185775, -9.686084310752812954 ) ) ;
#2026=CARTESIAN_POINT ( 'NONE',  ( -5.999999999999999112, 6.928203230275505220, -8.505011083697294083 ) ) ;
#2028=ORIENTED_EDGE ( 'NONE', *, *, #4781, .F. ) ;
#2029=ORIENTED_EDGE ( 'NONE', *, *, #3025, .F. ) ;
#2034=ORIENTED_EDGE ( 'NONE', *, *, #266, .F. ) ;
#2050=DIRECTION ( 'NONE',  ( -0.000000000000000000, -0.000000000000000000, 1.000000000000000000 ) ) ;
#2060=CARTESIAN_POINT ( 'NONE',  ( 0.000000000000000000, 0.000000000000000000, -0.6301867843887398735 ) ) ;
#2072=CARTESIAN_POINT ( 'NONE',  ( -2.822677224501521920, 8.762631390013995158, -8.969375302471101818 ) ) ;
#2073=CARTESIAN_POINT ( 'NONE',  ( 1.171714802207676431, -9.715814988945201236, -8.684787165853032675 ) ) ;
#2076=EDGE_CURVE ( 'NONE', #2978, #1856, #4066, .T. ) ;
#2077=ORIENTED_EDGE ( 'NONE', *, *, #3783, .T. ) ;
#2080=DIRECTION ( 'NONE',  ( -0.000000000000000000, -0.000000000000000000, 1.000000000000000000 ) ) ;
#2081=CARTESIAN_POINT ( 'NONE',  ( -9.000000000000000000, -3.792382572872301072, -8.707340555897303602 ) ) ;
#2084=CARTESIAN_POINT ( 'NONE',  ( 1.538998812063697930, 10.06940755529822695, -9.383905213720977301 ) ) ;
#2085=CARTESIAN_POINT ( 'NONE',  ( 9.000000000000000000, 0.4512186429437704538, -0.007346088320835161140 ) ) ;
#2091=EDGE_CURVE ( 'NONE', #5063, #3611, #2129, .T. ) ;
#2095=CARTESIAN_POINT ( 'NONE',  ( -7.546085493343360540, -6.035570354503548174, -0.5405968996908985247 ) ) ;
#2101=CARTESIAN_POINT ( 'NONE',  ( -9.000000000000000000, 1.973624059910456197, -8.465093423469367551 ) ) ;
#2104=CARTESIAN_POINT ( 'NONE',  ( 0.7403756379549473188, 10.54036220443051874, -9.525564194215789371 ) ) ;
#2105=CARTESIAN_POINT ( 'NONE',  ( 9.000000000000001776, 1.123146974283612654, -0.05788585198792846331 ) ) ;
#2108=CARTESIAN_POINT ( 'NONE',  ( 4.500000000000003553, -7.794228634059947147, 0.000000000000000000 ) ) ;
#2114=VERTEX_POINT ( 'NONE', #1811 ) ;
#2117=CARTESIAN_POINT ( 'NONE',  ( -9.000000000000000000, -5.196152422706636465, -1.199999999999999734 ) ) ;
#2120=DIRECTION ( 'NONE',  ( 1.000000000000000000, 0.000000000000000000, 0.000000000000000000 ) ) ;
#2124=CARTESIAN_POINT ( 'NONE',  ( -4.500000000000002665, -7.794228634059946259, 0.000000000000000000 ) ) ;
#2127=( NAMED_UNIT ( * ) PLANE_ANGLE_UNIT ( ) SI_UNIT ( $, .RADIAN. ) );
#2129=CIRCLE ( 'NONE', #2748, 12.38940648156203927 ) ;
#2134=CONICAL_SURFACE ( 'NONE', #4922, 9.000000000000001776, 0.8594454914424796144 ) ;
#2136=EDGE_CURVE ( 'NONE', #1856, #3771, #2563, .T. ) ;
#2137=CIRCLE ( 'NONE', #4158, 12.07201791628681420 ) ;
#2144=EDGE_CURVE ( 'NONE', #3920, #4400, #2299, .T. ) ;
#2149=CARTESIAN_POINT ( 'NONE',  ( -9.564083412974085263, 5.456344092479594288, -9.698321917585790430 ) ) ;
#2153=FACE_OUTER_BOUND ( 'NONE', #1589, .T. ) ;
#2155=DIRECTION ( 'NONE',  ( 0.000000000000000000, 0.000000000000000000, -1.000000000000000000 ) ) ;
#2157=DIRECTION ( 'NONE',  ( -0.000000000000000000, -0.000000000000000000, -1.000000000000000000 ) ) ;
#2158=EDGE_LOOP ( 'NONE', ( #1743, #3423, #235, #2077 ) ) ;
#2159=CARTESIAN_POINT ( 'NONE',  ( -9.000000000000000000, -0.9276453582363817230, -8.460808235231727537 ) ) ;
#2165=CARTESIAN_POINT ( 'NONE',  ( 9.562637692001345613, 5.457160213363109413, -9.698012095152311218 ) ) ;
#2168=CARTESIAN_POINT ( 'NONE',  ( 9.000000000000001776, -5.196152422706638241, -1.199999999999999734 ) ) ;
#2173=DIRECTION ( 'NONE',  ( 1.000000000000000000, 0.000000000000000000, 0.000000000000000000 ) ) ;
#2178=( BOUNDED_SURFACE ( )  B_SPLINE_SURFACE ( 3, 2, ( 
 ( #1989, #86, #1252 ),
 ( #2073, #4545, #4156 ),
 ( #2465, #492, #4129 ),
 ( #892, #3729, #2963 ),
 ( #1660, #5382, #2981 ),
 ( #3005, #1741, #824 ),
 ( #378, #5046, #3418 ),
 ( #31, #5069, #3339 ) ),
 .UNSPECIFIED., .F., .F., .T. ) 
 B_SPLINE_SURFACE_WITH_KNOTS ( ( 4, 2, 2, 4 ),
 ( 3, 3 ),
 ( 0.04613854442509285336, 0.05169925677048779755, 0.05447961294318526965, 0.05725996911588274174 ),
 ( 0.000000000000000000, 1.000000000000000000 ),
 .UNSPECIFIED. ) 
 GEOMETRIC_REPRESENTATION_ITEM ( )  RATIONAL_B_SPLINE_SURFACE ( (
 ( 1.000000000000000000, 0.8047781684971944127, 1.000000000000000000),
 ( 1.000000000000000000, 0.8123765127742887948, 1.000000000000000000),
 ( 1.000000000000000000, 0.8190661184400637174, 1.000000000000000000),
 ( 1.000000000000000000, 0.8191936944252291575, 1.000000000000000000),
 ( 1.000000000000000000, 0.8176092056339582248, 1.000000000000000000),
 ( 1.000000000000000000, 0.8122961334886901197, 1.000000000000000000),
 ( 1.000000000000000000, 0.8086310951057499308, 1.000000000000000000),
 ( 1.000000000000000000, 0.8047712311394933371, 1.000000000000000000) ) ) 
 REPRESENTATION_ITEM ( '' )  SURFACE ( )  );
#2181=CARTESIAN_POINT ( 'NONE',  ( 9.489636812669466792, -3.671909760406012246, -9.380312854821335478 ) ) ;
#2185=SURFACE_STYLE_USAGE ( .BOTH. , #2578 ) ;
#2191=CARTESIAN_POINT ( 'NONE',  ( 3.715604115503464921, 8.247099809125259640, -0.03002505116510094385 ) ) ;
#2192=CARTESIAN_POINT ( 'NONE',  ( 1.272360546691145400, 9.657707141273826679, -9.220334578152899141 ) ) ;
#2200=B_SPLINE_CURVE_WITH_KNOTS ( 'NONE', 3,
 ( #1430, #3112, #4756, #4045, #1949, #683, #4358, #4784 ),
 .UNSPECIFIED., .F., .F.,
 ( 4, 2, 2, 4 ),
 ( 2.475501736920113682E-07, 0.002666746755945494790, 0.003999996358831395607, 0.005333245961717295557 ),
 .UNSPECIFIED. ) ;
#2201=CARTESIAN_POINT ( 'NONE',  ( 0.000000000000000000, 0.000000000000000000, -12.00000000000000178 ) ) ;
#2220=DIRECTION ( 'NONE',  ( -0.000000000000000000, -0.000000000000000000, 1.000000000000000000 ) ) ;
#2224=CARTESIAN_POINT ( 'NONE',  ( -9.489636812669466792, 3.671909760406011358, -9.380312854821335478 ) ) ;
#2225=CIRCLE ( 'NONE', #2947, 6.000000000000000888 ) ;
#2234=CARTESIAN_POINT ( 'NONE',  ( -5.099999999999999645, 6.245698675651500839E-16, -0.6301867843887398735 ) ) ;
#2244=LINE ( 'NONE', #171, #1278 ) ;
#2253=ADVANCED_FACE ( 'NONE', ( #1104 ), #2541, .F. ) ;
#2257=CONICAL_SURFACE ( 'NONE', #6, 9.000000000000001776, 0.8594454914424796144 ) ;
#2276=EDGE_LOOP ( 'NONE', ( #1221, #1921, #369, #3384 ) ) ;
#2277=ORIENTED_EDGE ( 'NONE', *, *, #4271, .F. ) ;
#2285=ORIENTED_EDGE ( 'NONE', *, *, #1755, .F. ) ;
#2288=CARTESIAN_POINT ( 'NONE',  ( 3.049442433610978414E-16, 10.97743472985185775, -9.686084310752812954 ) ) ;
#2289=CARTESIAN_POINT ( 'NONE',  ( -9.000000000000000000, 5.196152422706629359, -12.00000000000000000 ) ) ;
#2299=B_SPLINE_CURVE_WITH_KNOTS ( 'NONE', 3,
 ( #2168, #5062, #887, #532, #3049, #3487, #2956, #2108 ),
 .UNSPECIFIED., .F., .F.,
 ( 4, 2, 2, 4 ),
 ( 2.475501736915396238E-07, 0.002666746755945493055, 0.003999996358831392138, 0.005333245961717292087 ),
 .UNSPECIFIED. ) ;
#2301=CARTESIAN_POINT ( 'NONE',  ( 9.000000000000000000, 0.9093366823532084142, -8.964884200296355132 ) ) ;
#2302=CARTESIAN_POINT ( 'NONE',  ( 5.099999999999999645, 0.000000000000000000, -12.00000000000000000 ) ) ;
#2303=AXIS2_PLACEMENT_3D ( 'NONE', #100, #4300, #2173 ) ;
#2310=ORIENTED_EDGE ( 'NONE', *, *, #563, .T. ) ;
#2317=CARTESIAN_POINT ( 'NONE',  ( -7.828285197792963501, -5.872642279174337787, -8.684787165848932844 ) ) ;
#2323=CARTESIAN_POINT ( 'NONE',  ( 0.000000000000000000, 0.000000000000000000, -11.07201791628681775 ) ) ;
#2326=CARTESIAN_POINT ( 'NONE',  ( -7.921880722261733787, 6.383959649155158900, -9.379910571084323578 ) ) ;
#2334=ORIENTED_EDGE ( 'NONE', *, *, #391, .T. ) ;
#2338=EDGE_CURVE ( 'NONE', #2607, #3420, #1443, .T. ) ;
#2347=CARTESIAN_POINT ( 'NONE',  ( -9.000000000000000000, 5.196152422706629359, -8.935996291721334472 ) ) ;
#2348=CARTESIAN_POINT ( 'NONE',  ( -2.893723230124264134, -8.721612959540728127, -9.019248292998303995 ) ) ;
#2349=CARTESIAN_POINT ( 'NONE',  ( 0.000000000000000000, 10.39230484541326760, -1.199999999999999734 ) ) ;
#2352=ORIENTED_EDGE ( 'NONE', *, *, #762, .F. ) ;
#2358=CARTESIAN_POINT ( 'NONE',  ( 0.000000000000000000, -10.39230484541327293, -8.935996291721338025 ) ) ;
#2359=( BOUNDED_SURFACE ( )  B_SPLINE_SURFACE ( 3, 2, ( 
 ( #476, #113, #2165 ),
 ( #1730, #94, #4267 ),
 ( #1367, #5033, #3349 ),
 ( #3407, #1672, #3835 ),
 ( #5081, #865, #1337 ),
 ( #1753, #2192, #2084 ),
 ( #527, #1295, #2104 ),
 ( #2532, #446, #5110 ) ),
 .UNSPECIFIED., .F., .F., .F. ) 
 B_SPLINE_SURFACE_WITH_KNOTS ( ( 4, 2, 2, 4 ),
 ( 3, 3 ),
 ( 0.04613854442509285336, 0.05169925677048779755, 0.05447961294318526965, 0.05725996911588274174 ),
 ( 0.000000000000000000, 1.000000000000000000 ),
 .UNSPECIFIED. ) 
 GEOMETRIC_REPRESENTATION_ITEM ( )  RATIONAL_B_SPLINE_SURFACE ( (
 ( 1.000000000000000000, 0.8047781684971936356, 1.000000000000000000),
 ( 1.000000000000000000, 0.8123765127741280345, 1.000000000000000000),
 ( 1.000000000000000000, 0.8190661184402779904, 1.000000000000000000),
 ( 1.000000000000000000, 0.8191936944251213548, 1.000000000000000000),
 ( 1.000000000000000000, 0.8176092056339585579, 1.000000000000000000),
 ( 1.000000000000000000, 0.8122961334886904528, 1.000000000000000000),
 ( 1.000000000000000000, 0.8086310951057497087, 1.000000000000000000),
 ( 1.000000000000000000, 0.8047712311394934481, 1.000000000000000000) ) ) 
 REPRESENTATION_ITEM ( '' )  SURFACE ( )  );
#2370=ADVANCED_FACE ( 'NONE', ( #2864 ), #4509, .T. ) ;
#2371=ORIENTED_EDGE ( 'NONE', *, *, #3216, .F. ) ;
#2374=CARTESIAN_POINT ( 'NONE',  ( 0.3349232592648707096, -10.58567287930771350, -9.544071379897779650 ) ) ;
#2379=ORIENTED_EDGE ( 'NONE', *, *, #1755, .T. ) ;
#2395=CIRCLE ( 'NONE', #3619, 9.000000000000001776 ) ;
#2402=CARTESIAN_POINT ( 'NONE',  ( 9.506737344437272696, -5.488717364925930653, -9.686084310752812954 ) ) ;
#2408=FACE_OUTER_BOUND ( 'NONE', #3454, .T. ) ;
#2409=PRODUCT_DEFINITION_SHAPE ( 'NONE', 'NONE',  #182 ) ;
#2417=CARTESIAN_POINT ( 'NONE',  ( -1.899904140753538487E-15, -10.46021122251003277, -9.269271692759762260 ) ) ;
#2420=CARTESIAN_POINT ( 'NONE',  ( 0.7810345657019077681, 10.51638858288773015, -9.518277236634762772 ) ) ;
#2434=CARTESIAN_POINT ( 'NONE',  ( 0.000000000000000000, 0.000000000000000000, 0.000000000000000000 ) ) ;
#2436=CIRCLE ( 'NONE', #3125, 9.000000000000001776 ) ;
#2441=CARTESIAN_POINT ( 'NONE',  ( 9.506737344437272696, 5.488717364925924436, -9.686084310752812954 ) ) ;
#2448=CARTESIAN_POINT ( 'NONE',  ( 6.329281523778166552, 7.289348427314501500, -9.189707035345829667 ) ) ;
#2449=EDGE_CURVE ( 'NONE', #428, #3262, #811, .T. ) ;
#2451=CARTESIAN_POINT ( 'NONE',  ( -1.500000000000000444, 9.526279441628826561, -8.667800885990208926 ) ) ;
#2456=ORIENTED_EDGE ( 'NONE', *, *, #1341, .T. ) ;
#2463=CARTESIAN_POINT ( 'NONE',  ( 0.4165158504820782315, 10.63278038381083945, -9.021433408186453562 ) ) ;
#2464=CARTESIAN_POINT ( 'NONE',  ( 0.000000000000000000, 0.000000000000000000, 0.000000000000000000 ) ) ;
#2465=CARTESIAN_POINT ( 'NONE',  ( 2.790577774332637429, -8.781164016207737788, -8.465119797811231805 ) ) ;
#2467=EDGE_CURVE ( 'NONE', #3611, #5063, #1865, .T. ) ;
#2472=CARTESIAN_POINT ( 'NONE',  ( 7.923304691439484237, 6.383148552592245117, -9.380055053747694771 ) ) ;
#2477=ORIENTED_EDGE ( 'NONE', *, *, #728, .F. ) ;
#2494=AXIS2_PLACEMENT_3D ( 'NONE', #1451, #3153, #1055 ) ;
#2499=CARTESIAN_POINT ( 'NONE',  ( -9.473648099969723901, -0.9041442221342959051, -9.137386922016339952 ) ) ;
#2502=ADVANCED_FACE ( 'NONE', ( #3381 ), #2134, .T. ) ;
#2503=TOROIDAL_SURFACE ( 'NONE', #3806, 12.07201791628681598, 0.9279820837131842470 ) ;
#2507=CARTESIAN_POINT ( 'NONE',  ( 0.7813822207450755730, -10.51618336147352295, -9.518202542148555878 ) ) ;
#2508=ORIENTED_EDGE ( 'NONE', *, *, #737, .T. ) ;
#2509=VERTEX_POINT ( 'NONE', #21 ) ;
#2516=ADVANCED_FACE ( 'NONE', ( #3043 ), #2359, .F. ) ;
#2517=B_SPLINE_CURVE_WITH_KNOTS ( 'NONE', 3,
 ( #4000, #626, #250, #1879, #168, #980, #3883, #2655 ),
 .UNSPECIFIED., .F., .F.,
 ( 4, 2, 2, 4 ),
 ( 0.007274027330054943195, 0.008608952725826013452, 0.009943878121597081107, 0.01261372891313921468 ),
 .UNSPECIFIED. ) ;
#2518=EDGE_CURVE ( 'NONE', #1856, #2978, #4073, .T. ) ;
#2522=CARTESIAN_POINT ( 'NONE',  ( -9.000000000000001776, -4.785828667975444262, -1.023175036954117711 ) ) ;
#2524=B_SPLINE_CURVE_WITH_KNOTS ( 'NONE', 3,
 ( #1183, #2825, #4506, #3234, #3171, #4824, #4032, #697, #2358 ),
 .UNSPECIFIED., .F., .F.,
 ( 4, 2, 1, 2, 4 ),
 ( 0.000000000000000000, 0.002598076211353316737, 0.005196152422706633474, 0.007794228634059948910, 0.01039230484541326521 ),
 .UNSPECIFIED. ) ;
#2526=CARTESIAN_POINT ( 'NONE',  ( -1.301042606982605321E-14, -10.39230484541326760, -1.199999999999999734 ) ) ;
#2527=CARTESIAN_POINT ( 'NONE',  ( -2.951638237467835602, 8.688175714460818710, -0.1192015822679155373 ) ) ;
#2528=CARTESIAN_POINT ( 'NONE',  ( -9.498409640465782289, -4.629036869500566809, -9.525571706933844141 ) ) ;
#2529=VERTEX_POINT ( 'NONE', #3428 ) ;
#2532=CARTESIAN_POINT ( 'NONE',  ( -0.4179773697347383132, 10.63362419234479006, -9.021743230619932774 ) ) ;
#2534=VERTEX_POINT ( 'NONE', #957 ) ;
#2538=ORIENTED_EDGE ( 'NONE', *, *, #1792, .T. ) ;
#2541=( BOUNDED_SURFACE ( )  B_SPLINE_SURFACE ( 3, 2, ( 
 ( #606, #4830, #3127 ),
 ( #1935, #3094, #4370 ),
 ( #230, #1470, #3945 ),
 ( #633, #2301, #666 ),
 ( #4033, #1886, #4771 ),
 ( #1050, #256, #5141 ),
 ( #2718, #2744, #4008 ),
 ( #4350, #175, #3070 ) ),
 .UNSPECIFIED., .F., .F., .F. ) 
 B_SPLINE_SURFACE_WITH_KNOTS ( ( 4, 2, 2, 4 ),
 ( 3, 3 ),
 ( 0.04599591305096960986, 0.05155656099146234406, 0.05433688496170870769, 0.05711720893195507132 ),
 ( 0.000000000000000000, 1.000000000000000000 ),
 .UNSPECIFIED. ) 
 GEOMETRIC_REPRESENTATION_ITEM ( )  RATIONAL_B_SPLINE_SURFACE ( (
 ( 1.000000000000000000, 0.8047781771973553377, 1.000000000000000000),
 ( 1.000000000000000000, 0.8123762916867537376, 1.000000000000000000),
 ( 1.000000000000000000, 0.8190655187926852987, 1.000000000000000000),
 ( 1.000000000000000000, 0.8191939758637984959, 1.000000000000000000),
 ( 1.000000000000000000, 0.8176095670996671450, 1.000000000000000000),
 ( 1.000000000000000000, 0.8122963966407920067, 1.000000000000000000),
 ( 1.000000000000000000, 0.8086312082325360917, 1.000000000000000000),
 ( 1.000000000000000000, 0.8047712221770487728, 1.000000000000000000) ) ) 
 REPRESENTATION_ITEM ( '' )  SURFACE ( )  );
#2542=CARTESIAN_POINT ( 'NONE',  ( 0.000000000000000000, 0.000000000000000000, 0.000000000000000000 ) ) ;
#2543=EDGE_CURVE ( 'NONE', #2607, #2534, #5001, .T. ) ;
#2544=CARTESIAN_POINT ( 'NONE',  ( 0.3334815747005966946, 10.58484052233643524, -9.543752552345290852 ) ) ;
#2548=DIRECTION ( 'NONE',  ( 1.000000000000000000, 0.000000000000000000, 0.000000000000000000 ) ) ;
#2554=CARTESIAN_POINT ( 'NONE',  ( 7.500000000000000000, -6.062177826491074839, -8.667800885990210702 ) ) ;
#2563=LINE ( 'NONE', #1342, #3179 ) ;
#2569=CARTESIAN_POINT ( 'NONE',  ( -1.219033264612565448, 9.688495661947332138, -9.200452032552545845 ) ) ;
#2570=CARTESIAN_POINT ( 'NONE',  ( 0.000000000000000000, 0.000000000000000000, -25.03750572909317285 ) ) ;
#2571=AXIS2_PLACEMENT_3D ( 'NONE', #2201, #3775, #2120 ) ;
#2576=CARTESIAN_POINT ( 'NONE',  ( 0.000000000000000000, 10.39230484541326760, -1.199999999999999734 ) ) ;
#2578=SURFACE_SIDE_STYLE ('',( #68 ) ) ;
#2584=CARTESIAN_POINT ( 'NONE',  ( 0.000000000000000000, 0.000000000000000000, -11.97459999999999880 ) ) ;
#2590=DIRECTION ( 'NONE',  ( 1.000000000000000000, 0.000000000000000000, 0.000000000000000000 ) ) ;
#2591=AXIS2_PLACEMENT_3D ( 'NONE', #2289, #949, #1902 ) ;
#2607=VERTEX_POINT ( 'NONE', #3590 ) ;
#2610=ORIENTED_EDGE ( 'NONE', *, *, #4201, .T. ) ;
#2611=DIRECTION ( 'NONE',  ( -1.000000000000000000, 0.000000000000000000, 0.000000000000000000 ) ) ;
#2617=B_SPLINE_CURVE_WITH_KNOTS ( 'NONE', 3,
 ( #2526, #4204, #440, #1309, #5026, #1287, #2966, #2124 ),
 .UNSPECIFIED., .F., .F.,
 ( 4, 2, 2, 4 ),
 ( 2.475501737064928787E-07, 0.002666746755945506933, 0.003999996358831405148, 0.005333245961717304230 ),
 .UNSPECIFIED. ) ;
#2622=CARTESIAN_POINT ( 'NONE',  ( -9.000000000000001776, 0.2246546977803019485, 1.534188425714351489E-15 ) ) ;
#2623=CARTESIAN_POINT ( 'NONE',  ( 9.000000000000001776, 0.000000000000000000, 0.000000000000000000 ) ) ;
#2625=CYLINDRICAL_SURFACE ( 'NONE', #228, 6.000000000000000888 ) ;
#2649=CARTESIAN_POINT ( 'NONE',  ( -9.000000000000000000, -5.196152422706636465, -8.935996291721336249 ) ) ;
#2655=CARTESIAN_POINT ( 'NONE',  ( 9.000000000000001776, 0.000000000000000000, 0.000000000000000000 ) ) ;
#2670=ORIENTED_EDGE ( 'NONE', *, *, #4181, .F. ) ;
#2672=CONICAL_SURFACE ( 'NONE', #2757, 6.000000000000000000, 0.9599310885968784790 ) ;
#2677=B_SPLINE_CURVE_WITH_KNOTS ( 'NONE', 3,
 ( #783, #1642, #2417, #3321, #4549, #1604 ),
 .UNSPECIFIED., .F., .F.,
 ( 4, 2, 4 ),
 ( 0.000000000000000000, 0.0005027859236379837553, 0.001005571847275967511 ),
 .UNSPECIFIED. ) ;
#2680=ORIENTED_EDGE ( 'NONE', *, *, #266, .T. ) ;
#2683=DIRECTION ( 'NONE',  ( 1.000000000000000000, 0.000000000000000000, 0.000000000000000000 ) ) ;
#2693=DIRECTION ( 'NONE',  ( -1.000000000000000000, 0.000000000000000000, 0.000000000000000000 ) ) ;
#2695=ADVANCED_FACE ( 'NONE', ( #4796 ), #2672, .F. ) ;
#2696=B_SPLINE_CURVE_WITH_KNOTS ( 'NONE', 3,
 ( #5066, #3319, #967, #2224, #382, #5144 ),
 .UNSPECIFIED., .F., .F.,
 ( 4, 2, 4 ),
 ( 0.005538372264888902219, 0.008302394062588029644, 0.01106641586028715533 ),
 .UNSPECIFIED. ) ;
#2704=DIRECTION ( 'NONE',  ( -0.000000000000000000, -0.000000000000000000, 1.000000000000000000 ) ) ;
#2709=LINE ( 'NONE', #3082, #663 ) ;
#2713=DIRECTION ( 'NONE',  ( 1.000000000000000000, 0.000000000000000000, 0.000000000000000000 ) ) ;
#2714=DIRECTION ( 'NONE',  ( -1.000000000000000000, 0.000000000000000000, 0.000000000000000000 ) ) ;
#2715=LINE ( 'NONE', #628, #4928 ) ;
#2717=DIRECTION ( 'NONE',  ( -0.000000000000000000, -0.000000000000000000, 1.000000000000000000 ) ) ;
#2718=CARTESIAN_POINT ( 'NONE',  ( 9.000000000000000000, 4.737906595178606572, -8.848991057604585819 ) ) ;
#2719=CARTESIAN_POINT ( 'NONE',  ( -2.352990130084610634E-16, 10.39230484541326582, -8.935996291721336249 ) ) ;
#2721=EDGE_CURVE ( 'NONE', #3747, #5063, #3530, .T. ) ;
#2732=DIRECTION ( 'NONE',  ( 0.000000000000000000, 0.000000000000000000, -1.000000000000000000 ) ) ;
#2744=CARTESIAN_POINT ( 'NONE',  ( 8.999999999999998224, 4.659172099344154994, -9.367141211032262049 ) ) ;
#2748=AXIS2_PLACEMENT_3D ( 'NONE', #482, #2220, #2590 ) ;
#2751=FACE_BOUND ( 'NONE', #4970, .T. ) ;
#2756=CONICAL_SURFACE ( 'NONE', #3635, 5.010000000000002451, 0.9599310885968808105 ) ;
#2757=AXIS2_PLACEMENT_3D ( 'NONE', #604, #4319, #3091 ) ;
#2763=CARTESIAN_POINT ( 'NONE',  ( 9.473745496805529243, 1.478328004173170497E-13, -9.138786188337405747 ) ) ;
#2769=CARTESIAN_POINT ( 'NONE',  ( -0.7810345657019083232, -10.51638858288774259, -9.518277236634766325 ) ) ;
#2770=CARTESIAN_POINT ( 'NONE',  ( 3.049442433610978414E-16, 10.97743472985185775, -9.686084310752812954 ) ) ;
#2771=AXIS2_PLACEMENT_3D ( 'NONE', #1740, #3974, #1471 ) ;
#2782=CARTESIAN_POINT ( 'NONE',  ( -17.99999999999999645, -3.469446951953614189E-15, -12.00000000000000000 ) ) ;
#2787=FACE_OUTER_BOUND ( 'NONE', #1820, .T. ) ;
#2788=CARTESIAN_POINT ( 'NONE',  ( -3.954162315725865184, -8.656288888418751881, -9.137374534099176770 ) ) ;
#2801=CARTESIAN_POINT ( 'NONE',  ( 9.000000000000003553, 3.464101615137751722, -8.667800885990208926 ) ) ;
#2806=ORIENTED_EDGE ( 'NONE', *, *, #708, .T. ) ;
#2808=ORIENTED_EDGE ( 'NONE', *, *, #2721, .T. ) ;
#2812=B_SPLINE_CURVE_WITH_KNOTS ( 'NONE', 3,
 ( #4795, #3484, #549, #3886, #3965, #2191, #222, #3861 ),
 .UNSPECIFIED., .F., .F.,
 ( 4, 2, 2, 4 ),
 ( 2.475501736912785259E-07, 0.002666746755945495657, 0.003999996358831399076, 0.005333245961717302495 ),
 .UNSPECIFIED. ) ;
#2814=VERTEX_POINT ( 'NONE', #4884 ) ;
#2817=DIRECTION ( 'NONE',  ( 1.000000000000000000, 0.000000000000000000, 0.000000000000000000 ) ) ;
#2825=CARTESIAN_POINT ( 'NONE',  ( -8.249999999999998224, -5.629165124598855208, -8.787392856021023491 ) ) ;
#2835=EDGE_LOOP ( 'NONE', ( #4044, #702, #2990, #1164, #1079 ) ) ;
#2848=CARTESIAN_POINT ( 'NONE',  ( -3.145560420647206978, -9.127459525683745412, -9.189462574975419074 ) ) ;
#2851=CARTESIAN_POINT ( 'NONE',  ( 12.38940648156203750, 0.000000000000000000, -10.20000000000000107 ) ) ;
#2856=CARTESIAN_POINT ( 'NONE',  ( 0.000000000000000000, 0.000000000000000000, -12.00000000000000000 ) ) ;
#2859=CARTESIAN_POINT ( 'NONE',  ( 8.716590831518757909, 5.934788533967490842, -9.518202542148554102 ) ) ;
#2864=FACE_OUTER_BOUND ( 'NONE', #1650, .T. ) ;
#2866=B_SPLINE_CURVE_WITH_KNOTS ( 'NONE', 3,
 ( #4510, #790, #2451, #4116, #368, #2026, #3712, #1613, #3302 ),
 .UNSPECIFIED., .F., .F.,
 ( 4, 2, 1, 2, 4 ),
 ( 0.000000000000000000, 0.002598076211353316737, 0.005196152422706633474, 0.007794228634059948910, 0.01039230484541326521 ),
 .UNSPECIFIED. ) ;
#2873=B_SPLINE_CURVE_WITH_KNOTS ( 'NONE', 3,
 ( #1327, #4650, #923, #2181, #3852, #105 ),
 .UNSPECIFIED., .F., .F.,
 ( 4, 2, 4 ),
 ( 0.005538372264888893545, 0.008302394062588022705, 0.01106641586028715360 ),
 .UNSPECIFIED. ) ;
#2890=LINE ( 'NONE', #3650, #5172 ) ;
#2892=DIRECTION ( 'NONE',  ( 0.000000000000000000, 0.000000000000000000, 1.000000000000000000 ) ) ;
#2905=EDGE_LOOP ( 'NONE', ( #3955, #2310, #3666, #3907, #3452, #444, #4149 ) ) ;
#2912=CYLINDRICAL_SURFACE ( 'NONE', #1723, 6.000000000000000888 ) ;
#2913=EDGE_CURVE ( 'NONE', #754, #3765, #2137, .T. ) ;
#2919=CARTESIAN_POINT ( 'NONE',  ( -9.000000000000000000, -3.727046135536770777, -9.220349054170952741 ) ) ;
#2926=ADVANCED_FACE ( 'NONE', ( #1606 ), #2503, .T. ) ;
#2928=EDGE_CURVE ( 'NONE', #5042, #1919, #3191, .T. ) ;
#2931=ORIENTED_EDGE ( 'NONE', *, *, #3062, .F. ) ;
#2937=DIRECTION ( 'NONE',  ( -0.000000000000000000, -0.000000000000000000, 1.000000000000000000 ) ) ;
#2939=AXIS2_PLACEMENT_3D ( 'NONE', #3273, #5009, #4563 ) ;
#2940=DIRECTION ( 'NONE',  ( 1.000000000000000000, 0.000000000000000000, 0.000000000000000000 ) ) ;
#2942=CARTESIAN_POINT ( 'NONE',  ( -6.000000000000000000, 0.000000000000000000, -11.97459999999999880 ) ) ;
#2943=CARTESIAN_POINT ( 'NONE',  ( -9.000000000000000000, 5.581228263432454817, -9.543753411584054547 ) ) ;
#2947=AXIS2_PLACEMENT_3D ( 'NONE', #90, #2157, #1746 ) ;
#2950=CARTESIAN_POINT ( 'NONE',  ( 0.000000000000000000, 0.000000000000000000, 0.000000000000000000 ) ) ;
#2953=ORIENTED_EDGE ( 'NONE', *, *, #4271, .T. ) ;
#2956=CARTESIAN_POINT ( 'NONE',  ( 4.894105558640191589, -7.566691683689909631, -3.942938369468767290E-15 ) ) ;
#2961=DIRECTION ( 'NONE',  ( 0.000000000000000000, 0.000000000000000000, 1.000000000000000000 ) ) ;
#2963=CARTESIAN_POINT ( 'NONE',  ( 5.519484922003871752, -7.752549460314996921, -9.137374534099006240 ) ) ;
#2966=CARTESIAN_POINT ( 'NONE',  ( -4.105894441359819069, -8.021765584429989104, -4.008159906407348416E-15 ) ) ;
#2974=EDGE_CURVE ( 'NONE', #2814, #3262, #274, .T. ) ;
#2977=EDGE_LOOP ( 'NONE', ( #3928, #267, #1298, #1611 ) ) ;
#2978=VERTEX_POINT ( 'NONE', #898 ) ;
#2981=CARTESIAN_POINT ( 'NONE',  ( 6.331831610933278398, -7.287864996261299133, -9.189462574975568288 ) ) ;
#2984=CARTESIAN_POINT ( 'NONE',  ( -9.000000000000000000, 1.787897550172801830, -0.1425508600568100859 ) ) ;
#2990=ORIENTED_EDGE ( 'NONE', *, *, #1481, .T. ) ;
#2991=CARTESIAN_POINT ( 'NONE',  ( -9.489862997586008930, -3.701980733639088417, -9.383919243293616930 ) ) ;
#3002=ORIENTED_EDGE ( 'NONE', *, *, #4409, .F. ) ;
#3005=CARTESIAN_POINT ( 'NONE',  ( 7.784221022415031221, -5.898082742690404778, -8.707326526324870031 ) ) ;
#3011=FACE_OUTER_BOUND ( 'NONE', #2905, .T. ) ;
#3014=AXIS2_PLACEMENT_3D ( 'NONE', #402, #4980, #4099 ) ;
#3025=EDGE_CURVE ( 'NONE', #1856, #1919, #5049, .T. ) ;
#3027=ORIENTED_EDGE ( 'NONE', *, *, #3277, .T. ) ;
#3028=CARTESIAN_POINT ( 'NONE',  ( -9.000000000000000000, -5.196152422706636465, -1.199999999999999734 ) ) ;
#3040=VERTEX_POINT ( 'NONE', #498 ) ;
#3043=FACE_OUTER_BOUND ( 'NONE', #26, .T. ) ;
#3049=CARTESIAN_POINT ( 'NONE',  ( 6.052010058236154677, -6.898175209152300091, -0.1432599722966034494 ) ) ;
#3053=FACE_OUTER_BOUND ( 'NONE', #3585, .T. ) ;
#3060=CARTESIAN_POINT ( 'NONE',  ( -9.000000000000005329, -1.732050807568881634, -8.505011083697297636 ) ) ;
#3062=EDGE_CURVE ( 'NONE', #5291, #745, #2225, .T. ) ;
#3070=CARTESIAN_POINT ( 'NONE',  ( 9.507374323136149386, 5.554569297917910653, -9.698322317877195786 ) ) ;
#3076=CARTESIAN_POINT ( 'NONE',  ( -9.000000000000000000, -5.196152422706636465, -8.935996291721336249 ) ) ;
#3078=VERTEX_POINT ( 'NONE', #4205 ) ;
#3082=CARTESIAN_POINT ( 'NONE',  ( 0.000000000000000000, -10.39230484541327293, -12.00000000000000000 ) ) ;
#3087=VECTOR ( 'NONE', #4733, 1000.000000000000000 ) ;
#3091=DIRECTION ( 'NONE',  ( -1.000000000000000000, 0.000000000000000000, 0.000000000000000000 ) ) ;
#3094=CARTESIAN_POINT ( 'NONE',  ( 9.000000000000000000, -3.788589235757911844, -9.200462692535689158 ) ) ;
#3098=ADVANCED_FACE ( 'NONE', ( #3011 ), #1188, .T. ) ;
#3112=CARTESIAN_POINT ( 'NONE',  ( -8.281895533831891143, 5.610750229555061530, -0.8426663529491297266 ) ) ;
#3114=FACE_OUTER_BOUND ( 'NONE', #2977, .T. ) ;
#3119=ADVANCED_FACE ( 'NONE', ( #3114 ), #2625, .F. ) ;
#3121=CARTESIAN_POINT ( 'NONE',  ( -8.716590831518756133, -5.934788533967497948, -9.518202542148552325 ) ) ;
#3122=DIRECTION ( 'NONE',  ( 0.000000000000000000, 0.000000000000000000, 1.000000000000000000 ) ) ;
#3125=AXIS2_PLACEMENT_3D ( 'NONE', #4087, #2892, #2940 ) ;
#3126=EDGE_CURVE ( 'NONE', #3765, #5063, #1435, .T. ) ;
#3127=CARTESIAN_POINT ( 'NONE',  ( 9.507358203129939511, -5.552904979773809480, -9.698011706630772721 ) ) ;
#3130=ORIENTED_EDGE ( 'NONE', *, *, #3874, .T. ) ;
#3136=DIRECTION ( 'NONE',  ( -0.8660254037844383745, 0.5000000000000003331, 0.000000000000000000 ) ) ;
#3137=CARTESIAN_POINT ( 'NONE',  ( -9.416515850482078065, -4.955676884309061947, -9.021433408186455338 ) ) ;
#3138=DIRECTION ( 'NONE',  ( -1.000000000000000000, 0.000000000000000000, 0.000000000000000000 ) ) ;
#3146=DIRECTION ( 'NONE',  ( 0.8191520442889902442, 1.003171929053522651E-16, -0.5735764363510483799 ) ) ;
#3151=CARTESIAN_POINT ( 'NONE',  ( -9.000000000000001776, 0.000000000000000000, 0.000000000000000000 ) ) ;
#3153=DIRECTION ( 'NONE',  ( 0.000000000000000000, 0.000000000000000000, -1.000000000000000000 ) ) ;
#3163=ADVANCED_FACE ( 'NONE', ( #3991 ), #597, .T. ) ;
#3164=ORIENTED_EDGE ( 'NONE', *, *, #737, .F. ) ;
#3166=DIRECTION ( 'NONE',  ( 0.8660254037844383745, -0.5000000000000003331, 0.000000000000000000 ) ) ;
#3169=DIRECTION ( 'NONE',  ( -1.000000000000000000, 0.000000000000000000, 0.000000000000000000 ) ) ;
#3171=CARTESIAN_POINT ( 'NONE',  ( -4.500000000000000000, -7.794228634059951588, -8.419403919045803875 ) ) ;
#3177=ORIENTED_EDGE ( 'NONE', *, *, #310, .T. ) ;
#3178=B_SPLINE_CURVE_WITH_KNOTS ( 'NONE', 3,
 ( #2288, #4021, #5261, #5149, #3956, #1869 ),
 .UNSPECIFIED., .F., .F.,
 ( 4, 2, 4 ),
 ( -5.636559625666465778E-06, 0.0004989239064927809787, 0.001003484372611228564 ),
 .UNSPECIFIED. ) ;
#3179=VECTOR ( 'NONE', #5113, 1000.000000000000000 ) ;
#3184=ORIENTED_EDGE ( 'NONE', *, *, #2974, .F. ) ;
#3186=PRODUCT_DEFINITION_FORMATION_WITH_SPECIFIED_SOURCE ( 'ANY', '', #976, .NOT_KNOWN. ) ;
#3191=CIRCLE ( 'NONE', #575, 6.000000000000000000 ) ;
#3192=ORIENTED_EDGE ( 'NONE', *, *, #3025, .T. ) ;
#3194=CARTESIAN_POINT ( 'NONE',  ( -2.865539685210635845, -8.737884736783355422, -8.512883888440837765 ) ) ;
#3209=B_SPLINE_CURVE_WITH_KNOTS ( 'NONE', 3,
 ( #2441, #3696, #1120, #713, #270, #2763 ),
 .UNSPECIFIED., .F., .F.,
 ( 4, 2, 4 ),
 ( 0.000000000000000000, 0.002769186132444446773, 0.005538372264888893545 ),
 .UNSPECIFIED. ) ;
#3210=DIRECTION ( 'NONE',  ( -0.000000000000000000, -0.000000000000000000, 1.000000000000000000 ) ) ;
#3211=DIRECTION ( 'NONE',  ( 1.000000000000000000, 0.000000000000000000, 0.000000000000000000 ) ) ;
#3214=EDGE_CURVE ( 'NONE', #5213, #5234, #416, .T. ) ;
#3216=EDGE_CURVE ( 'NONE', #2509, #3920, #1843, .T. ) ;
#3219=CARTESIAN_POINT ( 'NONE',  ( -9.473745496805529243, -1.478735707944909295E-13, -9.138786188337405747 ) ) ;
#3231=CARTESIAN_POINT ( 'NONE',  ( -3.945874696944569937, 8.661172281173762144, -9.138600484129256074 ) ) ;
#3234=CARTESIAN_POINT ( 'NONE',  ( -5.999999999999999112, -6.928203230275515878, -8.505011083697295859 ) ) ;
#3239=EDGE_LOOP ( 'NONE', ( #1245, #135, #4629, #2285, #4881 ) ) ;
#3242=EDGE_CURVE ( 'NONE', #3078, #1225, #2709, .T. ) ;
#3250=CARTESIAN_POINT ( 'NONE',  ( 8.283033339518244276, 5.610093317135758539, -0.8432325327665438630 ) ) ;
#3256=ORIENTED_EDGE ( 'NONE', *, *, #563, .F. ) ;
#3261=CARTESIAN_POINT ( 'NONE',  ( 5.527857873577811887, 7.747813868291101080, -9.138600484129261403 ) ) ;
#3262=VERTEX_POINT ( 'NONE', #2349 ) ;
#3265=DIRECTION ( 'NONE',  ( 0.000000000000000000, 0.000000000000000000, 1.000000000000000000 ) ) ;
#3266=CARTESIAN_POINT ( 'NONE',  ( 9.000000000000000000, 5.196152422706629359, -8.935996291721334472 ) ) ;
#3273=CARTESIAN_POINT ( 'NONE',  ( 0.000000000000000000, 0.000000000000000000, -12.00000000000000000 ) ) ;
#3277=EDGE_CURVE ( 'NONE', #2529, #4400, #1197, .T. ) ;
#3283=CARTESIAN_POINT ( 'NONE',  ( -8.603171985749405337, 5.425261183556192357, -8.848996304170942295 ) ) ;
#3287=VECTOR ( 'NONE', #3373, 1000.000000000000114 ) ;
#3288=( GEOMETRIC_REPRESENTATION_CONTEXT ( 3 ) GLOBAL_UNCERTAINTY_ASSIGNED_CONTEXT ( ( #3812 ) ) GLOBAL_UNIT_ASSIGNED_CONTEXT ( ( #3759, #3375, #500 ) ) REPRESENTATION_CONTEXT ( 'NONE', 'WORKASPACE' ) );
#3299=CIRCLE ( 'NONE', #3816, 6.000000000000000000 ) ;
#3301=DIRECTION ( 'NONE',  ( 1.000000000000000000, 0.000000000000000000, 0.000000000000000000 ) ) ;
#3302=CARTESIAN_POINT ( 'NONE',  ( -9.000000000000000000, 5.196152422706629359, -8.935996291721334472 ) ) ;
#3304=ORIENTED_EDGE ( 'NONE', *, *, #2091, .F. ) ;
#3312=ORIENTED_EDGE ( 'NONE', *, *, #2928, .F. ) ;
#3319=CARTESIAN_POINT ( 'NONE',  ( -9.473745496805527466, 0.9176529770164936206, -9.138786188337402194 ) ) ;
#3321=CARTESIAN_POINT ( 'NONE',  ( -1.020776138296702871E-15, -10.67487845244187206, -9.530716183751497539 ) ) ;
#3328=ORIENTED_EDGE ( 'NONE', *, *, #4657, .T. ) ;
#3337=LINE ( 'NONE', #4899, #4215 ) ;
#3338=CARTESIAN_POINT ( 'NONE',  ( -8.534985340083300898, 5.464628761784600997, -9.367146555589094703 ) ) ;
#3339=CARTESIAN_POINT ( 'NONE',  ( 9.564083412974087040, -5.456344092479600505, -9.698321917585792207 ) ) ;
#3344=CARTESIAN_POINT ( 'NONE',  ( 9.000000000000000000, -5.196152422706636465, -8.935996291721336249 ) ) ;
#3345=SHAPE_REPRESENTATION_RELATIONSHIP ( 'NONE' , 'NONE' ,  #1634, #1615 ) ;
#3349=CARTESIAN_POINT ( 'NONE',  ( 6.403089491456118054, 7.242747656091411024, -9.141698485140111075 ) ) ;
#3355=AXIS2_PLACEMENT_3D ( 'NONE', #87, #3850, #1284 ) ;
#3360=ORIENTED_EDGE ( 'NONE', *, *, #3277, .F. ) ;
#3361=CARTESIAN_POINT ( 'NONE',  ( 0.000000000000000000, 0.000000000000000000, 0.000000000000000000 ) ) ;
#3366=EDGE_CURVE ( 'NONE', #3420, #3747, #3209, .T. ) ;
#3373=DIRECTION ( 'NONE',  ( -0.8191520442889902442, 0.000000000000000000, -0.5735764363510483799 ) ) ;
#3375=( NAMED_UNIT ( * ) PLANE_ANGLE_UNIT ( ) SI_UNIT ( $, .RADIAN. ) );
#3381=FACE_OUTER_BOUND ( 'NONE', #5315, .T. ) ;
#3382=CARTESIAN_POINT ( 'NONE',  ( 1.566316456955013869, -10.05335742100714747, -9.380055053747698324 ) ) ;
#3383=VERTEX_POINT ( 'NONE', #5263 ) ;
#3384=ORIENTED_EDGE ( 'NONE', *, *, #4429, .F. ) ;
#3393=CARTESIAN_POINT ( 'NONE',  ( -8.038218111920156501E-16, -10.97743472985186486, -9.686084310752816506 ) ) ;
#3404=APPLICATION_CONTEXT ( 'automotive_design' ) ;
#3407=CARTESIAN_POINT ( 'NONE',  ( 3.696995237865069228, 8.257843649639102779, -8.460795847313656637 ) ) ;
#3408=CARTESIAN_POINT ( 'NONE',  ( 5.536779885055386430, -7.742692678355775904, -9.138972935415381471 ) ) ;
#3409=CARTESIAN_POINT ( 'NONE',  ( 0.000000000000000000, 0.000000000000000000, -11.34441321561125626 ) ) ;
#3412=ORIENTED_EDGE ( 'NONE', *, *, #3242, .F. ) ;
#3418=CARTESIAN_POINT ( 'NONE',  ( 8.758033615148258733, -5.911365213025767673, -9.525564194215363045 ) ) ;
#3420=VERTEX_POINT ( 'NONE', #412 ) ;
#3423=ORIENTED_EDGE ( 'NONE', *, *, #4421, .T. ) ;
#3428=CARTESIAN_POINT ( 'NONE',  ( -4.500000000000002665, -7.794228634059946259, 0.000000000000000000 ) ) ;
#3429=DIRECTION ( 'NONE',  ( 0.000000000000000000, 0.000000000000000000, -1.000000000000000000 ) ) ;
#3441=FACE_OUTER_BOUND ( 'NONE', #2158, .T. ) ;
#3442=AXIS2_PLACEMENT_3D ( 'NONE', #4110, #3701, #3166 ) ;
#3452=ORIENTED_EDGE ( 'NONE', *, *, #1832, .T. ) ;
#3454=EDGE_LOOP ( 'NONE', ( #3177, #867, #1490, #2028 ) ) ;
#3458=CARTESIAN_POINT ( 'NONE',  ( 3.945874696944568161, -8.661172281173767473, -9.138600484129261403 ) ) ;
#3460=EDGE_CURVE ( 'NONE', #3262, #3466, #2812, .T. ) ;
#3466=VERTEX_POINT ( 'NONE', #5109 ) ;
#3469=FACE_OUTER_BOUND ( 'NONE', #5077, .T. ) ;
#3476=DIRECTION ( 'NONE',  ( 0.000000000000000000, -1.000000000000000000, 0.000000000000000000 ) ) ;
#3477=ORIENTED_EDGE ( 'NONE', *, *, #3460, .T. ) ;
#3481=EDGE_CURVE ( 'NONE', #2978, #5042, #2715, .T. ) ;
#3482=CARTESIAN_POINT ( 'NONE',  ( 1.453914506656636574, -9.552886913616360332, -0.5405968996909029656 ) ) ;
#3484=CARTESIAN_POINT ( 'NONE',  ( 0.7181044661681106334, 9.977707038564833653, -0.8426663529491311699 ) ) ;
#3487=CARTESIAN_POINT ( 'NONE',  ( 5.284395884496541740, -7.341357458994639984, -0.03002505116510583924 ) ) ;
#3497=CARTESIAN_POINT ( 'NONE',  ( -9.000000000000000000, 3.464101615137751278, -8.667800885990208926 ) ) ;
#3504=DIRECTION ( 'NONE',  ( 0.9396926207859145341, 1.150791560227857665E-16, -0.3420201433256521151 ) ) ;
#3505=DIRECTION ( 'NONE',  ( 0.000000000000000000, 0.000000000000000000, -1.000000000000000000 ) ) ;
#3529=EDGE_CURVE ( 'NONE', #4754, #3040, #2244, .T. ) ;
#3530=LINE ( 'NONE', #173, #4236 ) ;
#3542=EDGE_CURVE ( 'NONE', #5213, #3383, #5187, .T. ) ;
#3546=STYLED_ITEM('',(#5433),#3657);
#3571=ORIENTED_EDGE ( 'NONE', *, *, #3366, .T. ) ;
#3579=CARTESIAN_POINT ( 'NONE',  ( -9.058806161333684770, 5.230104175782638087, -9.269265075619308902 ) ) ;
#3580=CARTESIAN_POINT ( 'NONE',  ( -9.562637692001347389, -5.457160213363115631, -9.698012095152312995 ) ) ;
#3585=EDGE_LOOP ( 'NONE', ( #2610, #2456, #3856, #4020 ) ) ;
#3589=FACE_OUTER_BOUND ( 'NONE', #265, .T. ) ;
#3590=CARTESIAN_POINT ( 'NONE',  ( 9.000000000000000000, 5.196152422706629359, -8.935996291721334472 ) ) ;
#3591=CARTESIAN_POINT ( 'NONE',  ( 0.000000000000000000, 0.000000000000000000, -11.97459999999999880 ) ) ;
#3601=CARTESIAN_POINT ( 'NONE',  ( -9.506737344437272696, -5.488717364925931541, -9.686084310752812954 ) ) ;
#3607=CARTESIAN_POINT ( 'NONE',  ( -3.712196824332475664, -8.249067009600855371, -8.964894084810355324 ) ) ;
#3610=EDGE_CURVE ( 'NONE', #1655, #4965, #467, .T. ) ;
#3611=VERTEX_POINT ( 'NONE', #4420 ) ;
#3615=CARTESIAN_POINT ( 'NONE',  ( -6.332118058842091557, 7.287734290476352683, -9.190020220263406259 ) ) ;
#3617=ADVANCED_FACE ( 'NONE', ( #3589 ), #3653, .F. ) ;
#3619=AXIS2_PLACEMENT_3D ( 'NONE', #180, #4805, #4408 ) ;
#3621=CARTESIAN_POINT ( 'NONE',  ( 9.000000000000000000, -5.196152422706636465, -8.935996291721336249 ) ) ;
#3623=ORIENTED_EDGE ( 'NONE', *, *, #4201, .F. ) ;
#3626=AXIS2_PLACEMENT_3D ( 'NONE', #2782, #638, #3981 ) ;
#3629=ORIENTED_EDGE ( 'NONE', *, *, #5139, .F. ) ;
#3632=PLANE ( 'NONE',  #1170 ) ;
#3635=AXIS2_PLACEMENT_3D ( 'NONE', #4693, #2704, #1864 ) ;
#3642=CARTESIAN_POINT ( 'NONE',  ( -3.696995237864706851, -8.257843649639317718, -8.460795847314500406 ) ) ;
#3648=ORIENTED_EDGE ( 'NONE', *, *, #728, .T. ) ;
#3650=CARTESIAN_POINT ( 'NONE',  ( -6.000000000000000888, 7.347880794884120722E-16, -25.03750572909317285 ) ) ;
#3651=ORIENTED_EDGE ( 'NONE', *, *, #3126, .F. ) ;
#3653=PLANE ( 'NONE',  #1790 ) ;
#3657=MANIFOLD_SOLID_BREP ( 'EndChamfer', #4567 ) ;
#3661=CARTESIAN_POINT ( 'NONE',  ( 8.999999999999996447, 4.330127018922190985, -8.787392856021021714 ) ) ;
#3666=ORIENTED_EDGE ( 'NONE', *, *, #4375, .T. ) ;
#3672=CARTESIAN_POINT ( 'NONE',  ( 6.000000000000000000, 7.347880794884119736E-16, -11.97459999999999880 ) ) ;
#3684=CARTESIAN_POINT ( 'NONE',  ( 9.000000000000001776, -4.330127018922196314, -8.787392856021023491 ) ) ;
#3690=ADVANCED_FACE ( 'NONE', ( #14 ), #415, .T. ) ;
#3693=ORIENTED_EDGE ( 'NONE', *, *, #2144, .F. ) ;
#3695=CARTESIAN_POINT ( 'NONE',  ( -1.272360546691562622, -9.657707141274665119, -9.220334578152071359 ) ) ;
#3696=CARTESIAN_POINT ( 'NONE',  ( 9.497968775322179980, 4.580952057516532783, -9.518120616476199558 ) ) ;
#3700=EDGE_CURVE ( 'NONE', #1225, #2529, #2617, .T. ) ;
#3701=DIRECTION ( 'NONE',  ( -0.5000000000000004441, -0.8660254037844384856, 0.000000000000000000 ) ) ;
#3710=ORIENTED_EDGE ( 'NONE', *, *, #1362, .F. ) ;
#3711=CARTESIAN_POINT ( 'NONE',  ( 0.000000000000000000, 0.000000000000000000, -10.20000000000000107 ) ) ;
#3712=CARTESIAN_POINT ( 'NONE',  ( -7.500000000000000000, 6.062177826491067734, -8.667800885990208926 ) ) ;
#3727=CARTESIAN_POINT ( 'NONE',  ( -7.784221022415209745, 5.898082742690295532, -8.707326526324866478 ) ) ;
#3729=CARTESIAN_POINT ( 'NONE',  ( 5.287803175666998534, -7.339390258519116195, -8.964894084810353547 ) ) ;
#3737=VECTOR ( 'NONE', #4309, 1000.000000000000000 ) ;
#3741=DIRECTION ( 'NONE',  ( 0.000000000000000000, 0.000000000000000000, -1.000000000000000000 ) ) ;
#3747=VERTEX_POINT ( 'NONE', #4724 ) ;
#3752=CARTESIAN_POINT ( 'NONE',  ( -7.950863337915141216, 6.367515845290393273, -9.383905213720927563 ) ) ;
#3756=( NAMED_UNIT ( * ) PLANE_ANGLE_UNIT ( ) SI_UNIT ( $, .RADIAN. ) );
#3757=DIRECTION ( 'NONE',  ( -0.000000000000000000, -0.000000000000000000, 1.000000000000000000 ) ) ;
#3759=( LENGTH_UNIT ( ) NAMED_UNIT ( * ) SI_UNIT ( .MILLI., .METRE. ) );
#3760=ORIENTED_EDGE ( 'NONE', *, *, #2091, .T. ) ;
#3763=CARTESIAN_POINT ( 'NONE',  ( -8.038218111920156501E-16, -10.97743472985186486, -9.686084310752816506 ) ) ;
#3764=ORIENTED_EDGE ( 'NONE', *, *, #3783, .F. ) ;
#3765=VERTEX_POINT ( 'NONE', #4676 ) ;
#3769=ORIENTED_EDGE ( 'NONE', *, *, #2913, .T. ) ;
#3771=VERTEX_POINT ( 'NONE', #2234 ) ;
#3773=CARTESIAN_POINT ( 'NONE',  ( -7.727639453308069228, 5.930750126845744319, -9.220334578152877825 ) ) ;
#3775=DIRECTION ( 'NONE',  ( -0.000000000000000000, -0.000000000000000000, 1.000000000000000000 ) ) ;
#3779=CARTESIAN_POINT ( 'NONE',  ( -9.000000000002474465, -4.659239318103709060, -9.367154206100524405 ) ) ;
#3783=EDGE_CURVE ( 'NONE', #3040, #2114, #3299, .T. ) ;
#3786=CARTESIAN_POINT ( 'NONE',  ( 9.000000000000000000, 2.225465271616588581, -0.2256151218434061245 ) ) ;
#3788=ORIENTED_EDGE ( 'NONE', *, *, #2076, .T. ) ;
#3791=CIRCLE ( 'NONE', #2571, 12.07201791628681420 ) ;
#3792=ORIENTED_EDGE ( 'NONE', *, *, #4019, .T. ) ;
#3797=CARTESIAN_POINT ( 'NONE',  ( -6.048361762532168839, -6.900281553659082689, -0.1192015822679202974 ) ) ;
#3798=AXIS2_PLACEMENT_3D ( 'NONE', #3409, #4615, #454 ) ;
#3802=CARTESIAN_POINT ( 'NONE',  ( -9.000000000000000000, 0.9001646245238090760, -0.03631462189738247914 ) ) ;
#3806=AXIS2_PLACEMENT_3D ( 'NONE', #4652, #2080, #924 ) ;
#3807=MECHANICAL_DESIGN_GEOMETRIC_PRESENTATION_REPRESENTATION('',(#491),#3288);
#3812=UNCERTAINTY_MEASURE_WITH_UNIT (LENGTH_MEASURE( 1.000000000000000082E-05 ), #3759, 'distance_accuracy_value', 'NONE');
#3813=CARTESIAN_POINT ( 'NONE',  ( 7.921880722261732011, -6.383959649155164229, -9.379910571084325355 ) ) ;
#3816=AXIS2_PLACEMENT_3D ( 'NONE', #541, #3878, #133 ) ;
#3822=CARTESIAN_POINT ( 'NONE',  ( -12.07201791628681598, 1.478395810043015094E-15, -11.07201791628681775 ) ) ;
#3827=ADVANCED_FACE ( 'NONE', ( #4079 ), #4841, .T. ) ;
#3828=CARTESIAN_POINT ( 'NONE',  ( -9.000000000000000000, 2.225465271616585472, -0.2256151218434065964 ) ) ;
#3830=ADVANCED_FACE ( 'NONE', ( #1545 ), #642, .F. ) ;
#3833=CARTESIAN_POINT ( 'NONE',  ( -8.999999999999998224, -1.854975783832116143, -9.019265669392103391 ) ) ;
#3835=CARTESIAN_POINT ( 'NONE',  ( 3.954162315725771482, 8.656288888417748240, -9.137374534098841039 ) ) ;
#3845=ORIENTED_EDGE ( 'NONE', *, *, #4897, .T. ) ;
#3850=DIRECTION ( 'NONE',  ( 0.000000000000000000, 0.000000000000000000, 1.000000000000000000 ) ) ;
#3852=CARTESIAN_POINT ( 'NONE',  ( 9.497981232281496489, -4.582241663078509220, -9.518359232022067573 ) ) ;
#3854=CARTESIAN_POINT ( 'NONE',  ( 0.000000000000000000, 0.000000000000000000, -10.20000000000000107 ) ) ;
#3856=ORIENTED_EDGE ( 'NONE', *, *, #4038, .T. ) ;
#3857=CARTESIAN_POINT ( 'NONE',  ( -9.000000000000000000, -0.9100846702111624609, -8.964906921228866565 ) ) ;
#3859=ORIENTED_EDGE ( 'NONE', *, *, #2543, .T. ) ;
#3861=CARTESIAN_POINT ( 'NONE',  ( 4.500000000000003553, 7.794228634059947147, 0.000000000000000000 ) ) ;
#3862=DIRECTION ( 'NONE',  ( -1.000000000000000000, 0.000000000000000000, 0.000000000000000000 ) ) ;
#3874=EDGE_CURVE ( 'NONE', #3466, #2534, #1424, .T. ) ;
#3878=DIRECTION ( 'NONE',  ( -0.000000000000000000, -0.000000000000000000, 1.000000000000000000 ) ) ;
#3879=CARTESIAN_POINT ( 'NONE',  ( 12.07201791628681598, 0.000000000000000000, -11.07201791628681775 ) ) ;
#3883=CARTESIAN_POINT ( 'NONE',  ( 9.000000000000000000, -0.9015406389697717682, 1.338312056661794536E-15 ) ) ;
#3886=CARTESIAN_POINT ( 'NONE',  ( 2.569563281917983666, 8.908766792898136444, -0.2264046624879769432 ) ) ;
#3906=CARTESIAN_POINT ( 'NONE',  ( -9.000000000000000000, -2.405731887095257756E-15, -8.419403919045802098 ) ) ;
#3907=ORIENTED_EDGE ( 'NONE', *, *, #233, .T. ) ;
#3919=CARTESIAN_POINT ( 'NONE',  ( 4.500000000000000000, 7.794228634059944483, -8.419403919045800322 ) ) ;
#3920=VERTEX_POINT ( 'NONE', #1281 ) ;
#3923=ADVANCED_FACE ( 'NONE', ( #1659 ), #1072, .F. ) ;
#3928=ORIENTED_EDGE ( 'NONE', *, *, #1667, .F. ) ;
#3937=CARTESIAN_POINT ( 'NONE',  ( 4.500000000000003553, -7.794228634059947147, 0.000000000000000000 ) ) ;
#3941=CARTESIAN_POINT ( 'NONE',  ( 6.000000000000000888, 0.000000000000000000, -25.03750572909317285 ) ) ;
#3945=CARTESIAN_POINT ( 'NONE',  ( 9.473949623761187766, -1.924001493855441725, -9.141718809717339411 ) ) ;
#3946=CARTESIAN_POINT ( 'NONE',  ( 0.7500000000000001110, 9.959292143521047080, -8.787392856021023491 ) ) ;
#3948=APPLICATION_CONTEXT ( 'automotive_design' ) ;
#3955=ORIENTED_EDGE ( 'NONE', *, *, #2721, .F. ) ;
#3956=CARTESIAN_POINT ( 'NONE',  ( -1.603504855002233253E-16, 10.39230484541326582, -9.106320693283315393 ) ) ;
#3959=CARTESIAN_POINT ( 'NONE',  ( 9.370348127520008674, -5.409973013826442134, -9.628763110917944346 ) ) ;
#3965=CARTESIAN_POINT ( 'NONE',  ( 2.947989941763847543, 8.690282058967600420, -0.1432599722965993694 ) ) ;
#3971=AXIS2_PLACEMENT_3D ( 'NONE', #4533, #789, #5362 ) ;
#3974=DIRECTION ( 'NONE',  ( -0.000000000000000000, -0.000000000000000000, 1.000000000000000000 ) ) ;
#3975=ORIENTED_EDGE ( 'NONE', *, *, #2913, .F. ) ;
#3981=DIRECTION ( 'NONE',  ( 1.000000000000000000, 0.000000000000000000, -0.000000000000000000 ) ) ;
#3990=CARTESIAN_POINT ( 'NONE',  ( -7.780966735391496414, -5.899961606181325813, -9.200452032553489090 ) ) ;
#3991=FACE_OUTER_BOUND ( 'NONE', #2835, .T. ) ;
#4000=CARTESIAN_POINT ( 'NONE',  ( 9.000000000000001776, -5.196152422706638241, -1.199999999999999734 ) ) ;
#4001=CARTESIAN_POINT ( 'NONE',  ( -6.329281523778169216, -7.289348427314507717, -9.189707035345833219 ) ) ;
#4002=CARTESIAN_POINT ( 'NONE',  ( -1.566316456955016090, 10.05335742100714036, -9.380055053747698324 ) ) ;
#4008=CARTESIAN_POINT ( 'NONE',  ( 9.498408982509888077, 4.628969134172655764, -9.525558946054186293 ) ) ;
#4019=EDGE_CURVE ( 'NONE', #2607, #428, #403, .T. ) ;
#4020=ORIENTED_EDGE ( 'NONE', *, *, #3529, .F. ) ;
#4021=CARTESIAN_POINT ( 'NONE',  ( 4.657533874636512748E-12, 10.81939018394125007, -9.628560800353234583 ) ) ;
#4029=CARTESIAN_POINT ( 'NONE',  ( -8.038218111920156501E-16, -10.97743472985186486, -9.686084310752816506 ) ) ;
#4032=CARTESIAN_POINT ( 'NONE',  ( -1.500000000000000666, -9.526279441628835443, -8.667800885990212478 ) ) ;
#4033=CARTESIAN_POINT ( 'NONE',  ( 9.000000000000000000, 1.887153537675259285, -8.512871225629151439 ) ) ;
#4037=ORIENTED_EDGE ( 'NONE', *, *, #310, .F. ) ;
#4038=EDGE_CURVE ( 'NONE', #2114, #3040, #1624, .T. ) ;
#4041=ORIENTED_EDGE ( 'NONE', *, *, #4019, .F. ) ;
#4042=FACE_OUTER_BOUND ( 'NONE', #4518, .T. ) ;
#4044=ORIENTED_EDGE ( 'NONE', *, *, #3542, .F. ) ;
#4045=CARTESIAN_POINT ( 'NONE',  ( -6.430436718082018110, 6.679690475221754298, -0.2264046624879764436 ) ) ;
#4046=CARTESIAN_POINT ( 'NONE',  ( -0.3968280142502572660, -10.16319608456390355, -8.848996304169316929 ) ) ;
#4051=AXIS2_PLACEMENT_3D ( 'NONE', #620, #4844, #3136 ) ;
#4052=ORIENTED_EDGE ( 'NONE', *, *, #4181, .T. ) ;
#4055=AXIS2_PLACEMENT_3D ( 'NONE', #3361, #1351, #4301 ) ;
#4058=CARTESIAN_POINT ( 'NONE',  ( -9.506737344437272696, 5.488717364925923548, -9.686084310752812954 ) ) ;
#4066=CIRCLE ( 'NONE', #3798, 5.099999999999999645 ) ;
#4067=AXIS2_PLACEMENT_3D ( 'NONE', #1115, #263, #4488 ) ;
#4073=CIRCLE ( 'NONE', #5369, 5.099999999999999645 ) ;
#4074=B_SPLINE_CURVE_WITH_KNOTS ( 'NONE', 3,
 ( #3937, #546, #1046, #3482, #1382, #655 ),
 .UNSPECIFIED., .F., .F.,
 ( 4, 2, 4 ),
 ( 0.005333245961717292087, 0.007986067645924077585, 0.01063888933013086222 ),
 .UNSPECIFIED. ) ;
#4079=FACE_OUTER_BOUND ( 'NONE', #1162, .T. ) ;
#4081=UNCERTAINTY_MEASURE_WITH_UNIT (LENGTH_MEASURE( 1.000000000000000082E-05 ), #4993, 'distance_accuracy_value', 'NONE');
#4083=AXIS2_PLACEMENT_3D ( 'NONE', #880, #2155, #856 ) ;
#4086=VERTEX_POINT ( 'NONE', #3151 ) ;
#4087=CARTESIAN_POINT ( 'NONE',  ( 0.000000000000000000, 0.000000000000000000, 0.000000000000000000 ) ) ;
#4089=CARTESIAN_POINT ( 'NONE',  ( 9.506737344437272696, 5.488717364925924436, -9.686084310752812954 ) ) ;
#4099=DIRECTION ( 'NONE',  ( 1.000000000000000000, 0.000000000000000000, 0.000000000000000000 ) ) ;
#4110=CARTESIAN_POINT ( 'NONE',  ( -9.000000000000000000, -5.196152422706636465, -12.00000000000000000 ) ) ;
#4116=CARTESIAN_POINT ( 'NONE',  ( -2.999999999999999112, 8.660254037844383745, -8.505011083697292307 ) ) ;
#4127=CARTESIAN_POINT ( 'NONE',  ( -6.331831610933253529, 7.287864996261684603, -9.189462574975657105 ) ) ;
#4129=CARTESIAN_POINT ( 'NONE',  ( 3.070858717647242386, -9.166611990350897798, -9.141698485139787778 ) ) ;
#4136=AXIS2_PLACEMENT_3D ( 'NONE', #2856, #4501, #34 ) ;
#4146=ORIENTED_EDGE ( 'NONE', *, *, #1898, .F. ) ;
#4149=ORIENTED_EDGE ( 'NONE', *, *, #2467, .T. ) ;
#4154=AXIS2_PLACEMENT_3D ( 'NONE', #2434, #5290, #769 ) ;
#4156=CARTESIAN_POINT ( 'NONE',  ( 1.499235438989850788, -10.09238013695879133, -9.361164777499757506 ) ) ;
#4158=AXIS2_PLACEMENT_3D ( 'NONE', #1217, #2050, #5356 ) ;
#4164=CARTESIAN_POINT ( 'NONE',  ( 3.000000000000000000, -8.660254037844392627, -8.505011083697295859 ) ) ;
#4165=VECTOR ( 'NONE', #3122, 1000.000000000000000 ) ;
#4169=CARTESIAN_POINT ( 'NONE',  ( -2.352990130084610634E-16, 10.39230484541326582, -12.00000000000000000 ) ) ;
#4180=CARTESIAN_POINT ( 'NONE',  ( -9.000000000000000000, -3.516072269208510903, -0.5641419778896283876 ) ) ;
#4181=EDGE_CURVE ( 'NONE', #2978, #4754, #1854, .T. ) ;
#4186=CARTESIAN_POINT ( 'NONE',  ( 1.500000000000000000, -9.526279441628833666, -8.667800885990210702 ) ) ;
#4201=EDGE_CURVE ( 'NONE', #4754, #3771, #4591, .T. ) ;
#4204=CARTESIAN_POINT ( 'NONE',  ( -0.7181044661681214025, -9.977707038564833653, -0.8426663529491328353 ) ) ;
#4205=CARTESIAN_POINT ( 'NONE',  ( 0.000000000000000000, -10.39230484541327293, -8.935996291721338025 ) ) ;
#4212=CARTESIAN_POINT ( 'NONE',  ( 9.000000000000001776, 0.000000000000000000, 0.000000000000000000 ) ) ;
#4213=B_SPLINE_CURVE_WITH_KNOTS ( 'NONE', 3,
 ( #4212, #426, #2085, #447, #2105, #4632, #3786, #1754, #4612, #885, #478, #905 ),
 .UNSPECIFIED., .F., .F.,
 ( 4, 2, 2, 2, 2, 4 ),
 ( 0.01261372891313921468, 0.01327902839800527111, 0.01394432788287132928, 0.01527492685260344214, 0.01660552582233555674, 0.01793612479206766960 ),
 .UNSPECIFIED. ) ;
#4215=VECTOR ( 'NONE', #2013, 999.9999999999998863 ) ;
#4225=CARTESIAN_POINT ( 'NONE',  ( 8.249999999999998224, 5.629165124598849879, -8.787392856021023491 ) ) ;
#4231=CARTESIAN_POINT ( 'NONE',  ( -8.999999999999998224, 0.4512186429437706758, -0.007346088320835175017 ) ) ;
#4233=DIRECTION ( 'NONE',  ( 1.000000000000000000, 0.000000000000000000, 0.000000000000000000 ) ) ;
#4235=PRESENTATION_STYLE_ASSIGNMENT (( #2185 ) ) ;
#4236=VECTOR ( 'NONE', #3504, 999.9999999999998863 ) ;
#4240=AXIS2_PLACEMENT_3D ( 'NONE', #3879, #3476, #2732 ) ;
#4260=CARTESIAN_POINT ( 'NONE',  ( -9.000000000000001776, 4.367518130255689357, -0.8586158810094310923 ) ) ;
#4265=CARTESIAN_POINT ( 'NONE',  ( 0.7500000000000001110, -9.959292143521054186, -8.787392856021027043 ) ) ;
#4267=CARTESIAN_POINT ( 'NONE',  ( 7.990639863760086392, 6.344566044897808510, -9.361164777499386247 ) ) ;
#4271=EDGE_CURVE ( 'NONE', #2509, #2607, #893, .T. ) ;
#4288=ORIENTED_EDGE ( 'NONE', *, *, #1481, .F. ) ;
#4300=DIRECTION ( 'NONE',  ( -0.000000000000000000, -0.000000000000000000, 1.000000000000000000 ) ) ;
#4301=DIRECTION ( 'NONE',  ( -1.000000000000000000, 0.000000000000000000, 0.000000000000000000 ) ) ;
#4309=DIRECTION ( 'NONE',  ( 0.000000000000000000, 0.000000000000000000, 1.000000000000000000 ) ) ;
#4310=CARTESIAN_POINT ( 'NONE',  ( 9.506737344437272696, -5.488717364925930653, -9.686084310752812954 ) ) ;
#4319=DIRECTION ( 'NONE',  ( 0.000000000000000000, 0.000000000000000000, -1.000000000000000000 ) ) ;
#4322=EDGE_CURVE ( 'NONE', #428, #5213, #2866, .T. ) ;
#4333=CIRCLE ( 'NONE', #4503, 5.099999999999999645 ) ;
#4340=ORIENTED_EDGE ( 'NONE', *, *, #937, .T. ) ;
#4350=CARTESIAN_POINT ( 'NONE',  ( 9.000000000000000000, 5.678793296733535279, -9.021743630911338130 ) ) ;
#4357=ORIENTED_EDGE ( 'NONE', *, *, #2338, .T. ) ;
#4358=CARTESIAN_POINT ( 'NONE',  ( -4.894105558640187148, 7.566691683689904302, 2.037114238146591921E-15 ) ) ;
#4366=CARTESIAN_POINT ( 'NONE',  ( -7.923304691439486014, -6.383148552592252223, -9.380055053747694771 ) ) ;
#4370=CARTESIAN_POINT ( 'NONE',  ( 9.489875848528154023, -3.747870292144412474, -9.361175357011155995 ) ) ;
#4372=ORIENTED_EDGE ( 'NONE', *, *, #3481, .T. ) ;
#4374=PLANE ( 'NONE',  #3626 ) ;
#4375=EDGE_CURVE ( 'NONE', #5361, #932, #4786, .T. ) ;
#4376=EDGE_LOOP ( 'NONE', ( #5088, #795, #3184 ) ) ;
#4378=CYLINDRICAL_SURFACE ( 'NONE', #4067, 5.099999999999999645 ) ;
#4384=CARTESIAN_POINT ( 'NONE',  ( -9.333481574700599026, -5.003616745783467046, -9.543752552345290852 ) ) ;
#4385=CARTESIAN_POINT ( 'NONE',  ( -9.000000000000000000, 4.330127018922190096, -8.787392856021023491 ) ) ;
#4390=DIRECTION ( 'NONE',  ( -0.000000000000000000, -0.000000000000000000, 1.000000000000000000 ) ) ;
#4391=DIRECTION ( 'NONE',  ( 0.000000000000000000, 0.000000000000000000, 1.000000000000000000 ) ) ;
#4400=VERTEX_POINT ( 'NONE', #4588 ) ;
#4406=FACE_OUTER_BOUND ( 'NONE', #4817, .T. ) ;
#4408=DIRECTION ( 'NONE',  ( 1.000000000000000000, 0.000000000000000000, 0.000000000000000000 ) ) ;
#4409=EDGE_CURVE ( 'NONE', #601, #2534, #4213, .T. ) ;
#4412=CARTESIAN_POINT ( 'NONE',  ( 4.500000000000003553, 7.794228634059947147, 0.000000000000000000 ) ) ;
#4420=CARTESIAN_POINT ( 'NONE',  ( -12.38940648156203750, 1.517264699098042146E-15, -10.20000000000000107 ) ) ;
#4421=EDGE_CURVE ( 'NONE', #3771, #4754, #4333, .T. ) ;
#4427=ORIENTED_EDGE ( 'NONE', *, *, #3542, .T. ) ;
#4429=EDGE_CURVE ( 'NONE', #745, #5042, #4797, .T. ) ;
#4434=DIRECTION ( 'NONE',  ( -0.8660254037844383745, -0.5000000000000003331, 0.000000000000000000 ) ) ;
#4435=CIRCLE ( 'NONE', #1131, 9.000000000000001776 ) ;
#4437=ORIENTED_EDGE ( 'NONE', *, *, #4608, .F. ) ;
#4439=CARTESIAN_POINT ( 'NONE',  ( 7.546085493343360540, 6.035570354503541068, -0.5405968996908940838 ) ) ;
#4445=DIRECTION ( 'NONE',  ( -0.000000000000000000, -0.000000000000000000, 1.000000000000000000 ) ) ;
#4451=CARTESIAN_POINT ( 'NONE',  ( 9.244715922125774199, 5.337439226220936028, -9.530716183751501092 ) ) ;
#4459=ADVANCED_FACE ( 'NONE', ( #193 ), #4746, .F. ) ;
#4462=CARTESIAN_POINT ( 'NONE',  ( 0.000000000000000000, 0.000000000000000000, 0.000000000000000000 ) ) ;
#4463=DIRECTION ( 'NONE',  ( 0.000000000000000000, 0.000000000000000000, 1.000000000000000000 ) ) ;
#4471=CARTESIAN_POINT ( 'NONE',  ( -9.058806161333684770, -5.230104175782646969, -9.269265075619308902 ) ) ;
#4472=AXIS2_PLACEMENT_3D ( 'NONE', #3822, #124, #513 ) ;
#4481=ORIENTED_EDGE ( 'NONE', *, *, #5118, .F. ) ;
#4488=DIRECTION ( 'NONE',  ( 1.000000000000000000, 0.000000000000000000, 0.000000000000000000 ) ) ;
#4501=DIRECTION ( 'NONE',  ( -0.000000000000000000, -0.000000000000000000, -1.000000000000000000 ) ) ;
#4503=AXIS2_PLACEMENT_3D ( 'NONE', #506, #3429, #5082 ) ;
#4505=ADVANCED_FACE ( 'NONE', ( #1020 ), #1802, .T. ) ;
#4506=CARTESIAN_POINT ( 'NONE',  ( -7.500000000000000000, -6.062177826491077504, -8.667800885990208926 ) ) ;
#4509=PLANE ( 'NONE',  #3971 ) ;
#4510=CARTESIAN_POINT ( 'NONE',  ( -2.352990130084610634E-16, 10.39230484541326582, -8.935996291721336249 ) ) ;
#4514=EDGE_LOOP ( 'NONE', ( #982, #1859, #322 ) ) ;
#4518=EDGE_LOOP ( 'NONE', ( #5056, #202, #4427, #3648, #4886 ) ) ;
#4520=CARTESIAN_POINT ( 'NONE',  ( -1.171714802207773687, 9.715814988945137287, -8.684787165852368318 ) ) ;
#4522=CARTESIAN_POINT ( 'NONE',  ( 3.049442433610978414E-16, 10.97743472985185775, -9.686084310752812954 ) ) ;
#4533=CARTESIAN_POINT ( 'NONE',  ( 0.000000000000000000, -10.39230484541327293, -12.00000000000000000 ) ) ;
#4538=EDGE_LOOP ( 'NONE', ( #1656, #4372, #4146, #2029 ) ) ;
#4545=CARTESIAN_POINT ( 'NONE',  ( 1.219033264610904554, -9.688495661941223247, -9.200452032562273175 ) ) ;
#4549=CARTESIAN_POINT ( 'NONE',  ( -1.388245801416654908E-12, -10.81994602764950386, -9.628763110917946122 ) ) ;
#4560=TOROIDAL_SURFACE ( 'NONE', #480, 12.07201791628681598, 0.9279820837131842470 ) ;
#4563=DIRECTION ( 'NONE',  ( 1.000000000000000000, 0.000000000000000000, 0.000000000000000000 ) ) ;
#4567=CLOSED_SHELL ( 'NONE', ( #5138, #4459, #5342, #3690, #1455, #1928, #5374, #1272, #618, #3617, #2370, #1617, #3163, #1315, #1889, #2926, #3098, #3827, #4505, #2502, #1014, #264, #1874, #3830, #5115, #4739, #2253, #3923, #2516, #1363, #2695, #3119 ) ) ;
#4570=VECTOR ( 'NONE', #4660, 1000.000000000000000 ) ;
#4580=CARTESIAN_POINT ( 'NONE',  ( -0.7169666604817549471, 9.978363950984137531, -0.8432325327665461945 ) ) ;
#4581=CARTESIAN_POINT ( 'NONE',  ( -9.477393160736850675, -1.839800711185081150, -9.189479368578805207 ) ) ;
#4588=CARTESIAN_POINT ( 'NONE',  ( 4.500000000000003553, -7.794228634059947147, 0.000000000000000000 ) ) ;
#4591=CIRCLE ( 'NONE', #1022, 5.099999999999999645 ) ;
#4599=DIRECTION ( 'NONE',  ( 1.000000000000000000, 0.000000000000000000, 0.000000000000000000 ) ) ;
#4601=CARTESIAN_POINT ( 'NONE',  ( -4.500000000000002665, -7.794228634059946259, 0.000000000000000000 ) ) ;
#4602=DIRECTION ( 'NONE',  ( -0.8191520442889915765, 1.003171929053524500E-16, 0.5735764363510464925 ) ) ;
#4608=EDGE_CURVE ( 'NONE', #4959, #5234, #4923, .T. ) ;
#4612=CARTESIAN_POINT ( 'NONE',  ( 8.999999999999998224, 3.519160108721334002, -0.5651793076691169482 ) ) ;
#4615=DIRECTION ( 'NONE',  ( -0.000000000000000000, -0.000000000000000000, 1.000000000000000000 ) ) ;
#4621=CARTESIAN_POINT ( 'NONE',  ( -8.283033339518246052, -5.610093317135764757, -0.8432325327665481929 ) ) ;
#4622=FACE_BOUND ( 'NONE', #4985, .T. ) ;
#4628=CARTESIAN_POINT ( 'NONE',  ( -9.000000000000000000, -1.887523386541274828, -8.512900682043403222 ) ) ;
#4629=ORIENTED_EDGE ( 'NONE', *, *, #708, .F. ) ;
#4632=CARTESIAN_POINT ( 'NONE',  ( 9.000000000000001776, 1.787897550172802275, -0.1425508600568101969 ) ) ;
#4633=EDGE_CURVE ( 'NONE', #4965, #3420, #1390, .T. ) ;
#4645=CARTESIAN_POINT ( 'NONE',  ( -9.000000000000000000, -5.196152422706636465, -1.199999999999999734 ) ) ;
#4650=CARTESIAN_POINT ( 'NONE',  ( 9.473745496805527466, -0.9176529770164938427, -9.138786188337402194 ) ) ;
#4652=CARTESIAN_POINT ( 'NONE',  ( 0.000000000000000000, 0.000000000000000000, -11.07201791628681775 ) ) ;
#4657=EDGE_CURVE ( 'NONE', #5234, #3078, #2524, .T. ) ;
#4660=DIRECTION ( 'NONE',  ( 0.000000000000000000, 0.000000000000000000, 1.000000000000000000 ) ) ;
#4674=LINE ( 'NONE', #895, #4713 ) ;
#4676=CARTESIAN_POINT ( 'NONE',  ( 12.07201791628681420, 0.000000000000000000, -12.00000000000000178 ) ) ;
#4679=CARTESIAN_POINT ( 'NONE',  ( 9.244715922125777752, -5.337439226220939581, -9.530716183751502868 ) ) ;
#4680=( LENGTH_UNIT ( ) NAMED_UNIT ( * ) SI_UNIT ( .MILLI., .METRE. ) );
#4693=CARTESIAN_POINT ( 'NONE',  ( 0.000000000000000000, 0.000000000000000000, -0.6932054628276118624 ) ) ;
#4695=EDGE_LOOP ( 'NONE', ( #1474, #155, #4052, #1962 ) ) ;
#4699=CARTESIAN_POINT ( 'NONE',  ( -9.000000000000005329, -4.330127018922199866, -8.787392856021028820 ) ) ;
#4700=CARTESIAN_POINT ( 'NONE',  ( 9.058808647644763568, -5.230105611255016385, -9.269271692759769365 ) ) ;
#4704=ORIENTED_EDGE ( 'NONE', *, *, #3216, .T. ) ;
#4713=VECTOR ( 'NONE', #4602, 1000.000000000000000 ) ;
#4724=CARTESIAN_POINT ( 'NONE',  ( 9.473745496805529243, 1.478328004173170497E-13, -9.138786188337405747 ) ) ;
#4725=DIRECTION ( 'NONE',  ( 0.000000000000000000, 0.000000000000000000, 1.000000000000000000 ) ) ;
#4729=CONICAL_SURFACE ( 'NONE', #2494, 9.000000000000001776, 0.8594454914424796144 ) ;
#4731=EDGE_LOOP ( 'NONE', ( #1297, #5207, #3623, #2670 ) ) ;
#4733=DIRECTION ( 'NONE',  ( 0.000000000000000000, 0.000000000000000000, 1.000000000000000000 ) ) ;
#4739=ADVANCED_FACE ( 'NONE', ( #4969 ), #511, .F. ) ;
#4742=CARTESIAN_POINT ( 'NONE',  ( 8.999999999999998224, 5.196152422706628471, -9.106324069981646119 ) ) ;
#4746=CONICAL_SURFACE ( 'NONE', #1717, 6.000000000000000000, 0.9599310885968784790 ) ;
#4754=VERTEX_POINT ( 'NONE', #91 ) ;
#4755=B_SPLINE_CURVE_WITH_KNOTS ( 'NONE', 3,
 ( #946, #2622, #4231, #3802, #1306, #2984, #3828, #1742, #922, #4260, #131, #1793 ),
 .UNSPECIFIED., .F., .F.,
 ( 4, 2, 2, 2, 2, 4 ),
 ( 0.01261372891313921468, 0.01327902839800527111, 0.01394432788287132755, 0.01527492685260344041, 0.01660552582233554980, 0.01793612479206766266 ),
 .UNSPECIFIED. ) ;
#4756=CARTESIAN_POINT ( 'NONE',  ( -7.552115898706446728, 6.032088698343841315, -0.5428950306860266251 ) ) ;
#4762=CARTESIAN_POINT ( 'NONE',  ( -9.000000000000000000, -5.196152422706636465, -12.00000000000000000 ) ) ;
#4765=B_SPLINE_CURVE_WITH_KNOTS ( 'NONE', 3,
 ( #4601, #437, #3797, #2095, #4621, #4645 ),
 .UNSPECIFIED., .F., .F.,
 ( 4, 2, 4 ),
 ( 0.005333245961717304230, 0.007986067645924081054, 0.01063888933013085701 ),
 .UNSPECIFIED. ) ;
#4771=CARTESIAN_POINT ( 'NONE',  ( 9.477391180807693161, 1.839439615276918794, -9.189449912164228351 ) ) ;
#4781=EDGE_CURVE ( 'NONE', #3078, #2509, #1526, .T. ) ;
#4784=CARTESIAN_POINT ( 'NONE',  ( -4.500000000000003553, 7.794228634059947147, 0.000000000000000000 ) ) ;
#4786=B_SPLINE_CURVE_WITH_KNOTS ( 'NONE', 3,
 ( #5034, #43, #3813, #1296, #3408, #3458, #96, #3382, #2507, #3763 ),
 .UNSPECIFIED., .F., .F.,
 ( 4, 2, 2, 2, 4 ),
 ( 0.000000000000000000, 0.002766603965071790135, 0.005533207930143580269, 0.008299811895215371271, 0.01106641586028716054 ),
 .UNSPECIFIED. ) ;
#4795=CARTESIAN_POINT ( 'NONE',  ( 0.000000000000000000, 10.39230484541326760, -1.199999999999999734 ) ) ;
#4796=FACE_OUTER_BOUND ( 'NONE', #613, .T. ) ;
#4797=LINE ( 'NONE', #3941, #857 ) ;
#4805=DIRECTION ( 'NONE',  ( 0.000000000000000000, 0.000000000000000000, 1.000000000000000000 ) ) ;
#4811=CARTESIAN_POINT ( 'NONE',  ( -9.369866752751233818, 5.409695091966935543, -9.628560800353236360 ) ) ;
#4812=CARTESIAN_POINT ( 'NONE',  ( -1.538998812064025667, -10.06940755529870302, -9.383905213721176253 ) ) ;
#4817=EDGE_LOOP ( 'NONE', ( #3710, #3975 ) ) ;
#4824=CARTESIAN_POINT ( 'NONE',  ( -2.999999999999998668, -8.660254037844394404, -8.505011083697297636 ) ) ;
#4830=CARTESIAN_POINT ( 'NONE',  ( 9.000000000000000000, -5.581221688749905319, -9.543752152530549537 ) ) ;
#4837=FACE_OUTER_BOUND ( 'NONE', #4514, .T. ) ;
#4841=CONICAL_SURFACE ( 'NONE', #1975, 9.000000000000001776, 0.8594454914424796144 ) ;
#4844=DIRECTION ( 'NONE',  ( 0.5000000000000004441, 0.8660254037844384856, -0.000000000000000000 ) ) ;
#4845=DIRECTION ( 'NONE',  ( -1.000000000000000000, 0.000000000000000000, 0.000000000000000000 ) ) ;
#4873=CARTESIAN_POINT ( 'NONE',  ( 5.284168072928040694, 7.341488986065032307, 1.982057096575062005E-15 ) ) ;
#4881=ORIENTED_EDGE ( 'NONE', *, *, #1832, .F. ) ;
#4882=CARTESIAN_POINT ( 'NONE',  ( 0.000000000000000000, 0.000000000000000000, 0.000000000000000000 ) ) ;
#4884=CARTESIAN_POINT ( 'NONE',  ( -4.500000000000003553, 7.794228634059947147, 0.000000000000000000 ) ) ;
#4885=CARTESIAN_POINT ( 'NONE',  ( -9.000000000000000000, -5.196152422706636465, -8.935996291721336249 ) ) ;
#4886=ORIENTED_EDGE ( 'NONE', *, *, #2974, .T. ) ;
#4897=EDGE_CURVE ( 'NONE', #2509, #5361, #1139, .T. ) ;
#4899=CARTESIAN_POINT ( 'NONE',  ( -12.38940648156203927, 0.000000000000000000, -10.20000000000000107 ) ) ;
#4914=CARTESIAN_POINT ( 'NONE',  ( 9.370348127518923320, 5.409973013828315302, -9.628763110917944346 ) ) ;
#4922=AXIS2_PLACEMENT_3D ( 'NONE', #2950, #73, #2611 ) ;
#4923=B_SPLINE_CURVE_WITH_KNOTS ( 'NONE', 3,
 ( #1524, #5335, #5309, #4471, #1100, #4885 ),
 .UNSPECIFIED., .F., .F.,
 ( 4, 2, 4 ),
 ( -5.636559625663623135E-06, 0.0004989239064927824966, 0.001003484372611228564 ),
 .UNSPECIFIED. ) ;
#4924=CARTESIAN_POINT ( 'NONE',  ( -6.000000000000000000, 0.000000000000000000, -11.97459999999999880 ) ) ;
#4928=VECTOR ( 'NONE', #3146, 1000.000000000000114 ) ;
#4959=VERTEX_POINT ( 'NONE', #1515 ) ;
#4962=CARTESIAN_POINT ( 'NONE',  ( -9.000000000000000000, -3.085342593989932158, -0.4353033105082920184 ) ) ;
#4965=VERTEX_POINT ( 'NONE', #4522 ) ;
#4969=FACE_OUTER_BOUND ( 'NONE', #3239, .T. ) ;
#4970=EDGE_LOOP ( 'NONE', ( #1566, #2931 ) ) ;
#4980=DIRECTION ( 'NONE',  ( -0.000000000000000000, -0.000000000000000000, 1.000000000000000000 ) ) ;
#4985=EDGE_LOOP ( 'NONE', ( #3764, #5055 ) ) ;
#4988=CARTESIAN_POINT ( 'NONE',  ( -9.417977369734735760, 4.954833075775106010, -9.021743230619930998 ) ) ;
#4989=FACE_OUTER_BOUND ( 'NONE', #2276, .T. ) ;
#4993=( LENGTH_UNIT ( ) NAMED_UNIT ( * ) SI_UNIT ( .MILLI., .METRE. ) );
#5001=LINE ( 'NONE', #1264, #4570 ) ;
#5003=EDGE_LOOP ( 'NONE', ( #3845, #3256, #690, #1230, #2277 ) ) ;
#5009=DIRECTION ( 'NONE',  ( 0.000000000000000000, 0.000000000000000000, 1.000000000000000000 ) ) ;
#5020=CARTESIAN_POINT ( 'NONE',  ( -9.000000000000001776, 0.000000000000000000, 0.000000000000000000 ) ) ;
#5026=CARTESIAN_POINT ( 'NONE',  ( -2.947989941763851984, -8.690282058967598644, -0.1432599722966032829 ) ) ;
#5032=ORIENTED_EDGE ( 'NONE', *, *, #3700, .F. ) ;
#5033=CARTESIAN_POINT ( 'NONE',  ( 6.177322775498883978, 6.825825878107829148, -8.969375302471100042 ) ) ;
#5034=CARTESIAN_POINT ( 'NONE',  ( 9.506737344437272696, -5.488717364925930653, -9.686084310752812954 ) ) ;
#5042=VERTEX_POINT ( 'NONE', #3672 ) ;
#5045=CARTESIAN_POINT ( 'NONE',  ( -6.106276769875783828, 6.866844308578849976, -9.019248292997451344 ) ) ;
#5046=CARTESIAN_POINT ( 'NONE',  ( 8.534985340083734329, -5.464628761784584121, -9.367146555587263279 ) ) ;
#5049=LINE ( 'NONE', #2942, #3287 ) ;
#5052=CARTESIAN_POINT ( 'NONE',  ( -9.489874121516242766, 3.747692455480259532, -9.361141881131302966 ) ) ;
#5055=ORIENTED_EDGE ( 'NONE', *, *, #4038, .F. ) ;
#5056=ORIENTED_EDGE ( 'NONE', *, *, #2449, .F. ) ;
#5057=CARTESIAN_POINT ( 'NONE',  ( 0.000000000000000000, 0.000000000000000000, -11.34441321561125626 ) ) ;
#5062=CARTESIAN_POINT ( 'NONE',  ( 8.281895533831889367, -5.610750229555068636, -0.8426663529491329463 ) ) ;
#5063=VERTEX_POINT ( 'NONE', #2851 ) ;
#5066=CARTESIAN_POINT ( 'NONE',  ( -9.473745496805529243, -1.478735707944909295E-13, -9.138786188337405747 ) ) ;
#5069=CARTESIAN_POINT ( 'NONE',  ( 9.334923259264868989, -5.002784388812196781, -9.544071379897776097 ) ) ;
#5073=CARTESIAN_POINT ( 'NONE',  ( 0.000000000000000000, 0.000000000000000000, -0.6932054628276118624 ) ) ;
#5077=EDGE_LOOP ( 'NONE', ( #5102, #1350, #2477 ) ) ;
#5078=CARTESIAN_POINT ( 'NONE',  ( -9.507374272674303128, -5.554564088132607047, -9.698321345470532151 ) ) ;
#5081=CARTESIAN_POINT ( 'NONE',  ( 2.865539685210587439, 8.737884736783376738, -8.512883888440002877 ) ) ;
#5082=DIRECTION ( 'NONE',  ( 1.000000000000000000, 0.000000000000000000, 0.000000000000000000 ) ) ;
#5085=CONICAL_SURFACE ( 'NONE', #4055, 9.000000000000001776, 0.8594454914424796144 ) ;
#5088=ORIENTED_EDGE ( 'NONE', *, *, #1177, .F. ) ;
#5102=ORIENTED_EDGE ( 'NONE', *, *, #1395, .F. ) ;
#5109=CARTESIAN_POINT ( 'NONE',  ( 4.500000000000003553, 7.794228634059947147, 0.000000000000000000 ) ) ;
#5110=CARTESIAN_POINT ( 'NONE',  ( -0.05670911061056357200, 11.01091124578873703, -9.698321917585792207 ) ) ;
#5113=DIRECTION ( 'NONE',  ( 0.000000000000000000, 0.000000000000000000, 1.000000000000000000 ) ) ;
#5115=ADVANCED_FACE ( 'NONE', ( #2408 ), #2178, .F. ) ;
#5118=EDGE_CURVE ( 'NONE', #1794, #4086, #689, .T. ) ;
#5138=ADVANCED_FACE ( 'NONE', ( #4989 ), #2912, .F. ) ;
#5139=EDGE_CURVE ( 'NONE', #2529, #1794, #4765, .T. ) ;
#5141=CARTESIAN_POINT ( 'NONE',  ( 9.489861534733870840, 3.701827684609153568, -9.383895017444986664 ) ) ;
#5143=EDGE_LOOP ( 'NONE', ( #3571, #2808, #3760, #2352, #2379, #1539, #815 ) ) ;
#5144=CARTESIAN_POINT ( 'NONE',  ( -9.506737344437272696, 5.488717364925923548, -9.686084310752812954 ) ) ;
#5146=CARTESIAN_POINT ( 'NONE',  ( -9.000000000000000000, 5.196152422706629359, -8.935996291721334472 ) ) ;
#5149=CARTESIAN_POINT ( 'NONE',  ( 3.040097435540409859E-15, 10.46020835156528683, -9.269265075619310679 ) ) ;
#5151=CARTESIAN_POINT ( 'NONE',  ( -9.000000000000001776, -3.464101615137761048, -8.667800885990210702 ) ) ;
#5166=CIRCLE ( 'NONE', #290, 9.000000000000001776 ) ;
#5172=VECTOR ( 'NONE', #4445, 1000.000000000000000 ) ;
#5177=CARTESIAN_POINT ( 'NONE',  ( -9.244707351836325415, 5.337434278162010770, -9.530707251625214482 ) ) ;
#5186=DIRECTION ( 'NONE',  ( 0.000000000000000000, 0.000000000000000000, -1.000000000000000000 ) ) ;
#5187=LINE ( 'NONE', #1439, #4165 ) ;
#5207=ORIENTED_EDGE ( 'NONE', *, *, #2136, .T. ) ;
#5213=VERTEX_POINT ( 'NONE', #5146 ) ;
#5234=VERTEX_POINT ( 'NONE', #3076 ) ;
#5236=CARTESIAN_POINT ( 'NONE',  ( 0.4179773697347388128, -10.63362419234479717, -9.021743230619936327 ) ) ;
#5248=DIRECTION ( 'NONE',  ( 0.000000000000000000, 0.000000000000000000, 1.000000000000000000 ) ) ;
#5256=CARTESIAN_POINT ( 'NONE',  ( -9.489595936502764673, -3.666866907830386157, -9.379652974972602308 ) ) ;
#5261=CARTESIAN_POINT ( 'NONE',  ( 3.854076807281087830E-15, 10.67486855632403220, -9.530707251625216259 ) ) ;
#5263=CARTESIAN_POINT ( 'NONE',  ( -9.000000000000000000, 5.196152422706629359, -1.199999999999997291 ) ) ;
#5267=PRODUCT_CONTEXT ( 'NONE', #3404, 'mechanical' ) ;
#5290=DIRECTION ( 'NONE',  ( 0.000000000000000000, 0.000000000000000000, 1.000000000000000000 ) ) ;
#5291=VERTEX_POINT ( 'NONE', #561 ) ;
#5299=AXIS2_PLACEMENT_3D ( 'NONE', #660, #3505, #174 ) ;
#5302=ORIENTED_EDGE ( 'NONE', *, *, #1469, .T. ) ;
#5306=CARTESIAN_POINT ( 'NONE',  ( -1.567730871772294865, -10.05252977580646601, -9.379910571084327131 ) ) ;
#5307=CARTESIAN_POINT ( 'NONE',  ( -5.536779885055386430, 7.742692678355767910, -9.138972935415379695 ) ) ;
#5309=CARTESIAN_POINT ( 'NONE',  ( -9.244707351836325415, -5.337434278162020540, -9.530707251625214482 ) ) ;
#5315=EDGE_LOOP ( 'NONE', ( #2034, #4481, #3629 ) ) ;
#5329=CARTESIAN_POINT ( 'NONE',  ( -9.506737344437272696, 5.488717364925923548, -9.686084310752812954 ) ) ;
#5335=CARTESIAN_POINT ( 'NONE',  ( -9.369866752750700911, -5.409695091967863689, -9.628560800353236360 ) ) ;
#5342=ADVANCED_FACE ( 'NONE', ( #3053 ), #2756, .F. ) ;
#5348=CARTESIAN_POINT ( 'NONE',  ( -9.334923259264868989, 5.002784388812189675, -9.544071379897774321 ) ) ;
#5356=DIRECTION ( 'NONE',  ( 1.000000000000000000, 0.000000000000000000, 0.000000000000000000 ) ) ;
#5361=VERTEX_POINT ( 'NONE', #2402 ) ;
#5362=DIRECTION ( 'NONE',  ( 0.8660254037844383745, 0.5000000000000003331, 0.000000000000000000 ) ) ;
#5369=AXIS2_PLACEMENT_3D ( 'NONE', #5057, #1696, #3862 ) ;
#5374=ADVANCED_FACE ( 'NONE', ( #240 ), #4378, .F. ) ;
#5382=CARTESIAN_POINT ( 'NONE',  ( 6.106276769875529808, -6.866844308578350820, -9.019248292997474437 ) ) ;
#5427=COLOUR_RGB('Black',0.12,0.14,0.17);
#5428=FILL_AREA_STYLE_COLOUR('',#5427);
#5429=FILL_AREA_STYLE('',(#5428));
#5430=SURFACE_STYLE_FILL_AREA(#5429);
#5431=SURFACE_SIDE_STYLE('',(#5430));
#5432=SURFACE_STYLE_USAGE(.BOTH.,#5431);
#5433=PRESENTATION_STYLE_ASSIGNMENT((#5432));
ENDSEC;
END-ISO-10303-21;
